ISO-10303-21;
HEADER;
FILE_DESCRIPTION (('STEP AP214'),
    '1' );
FILE_NAME ('Cage Hanger.step',
    '2026-10-12T23:53:07',
    ( '' ),
    ( '' ),
    'SwSTEP 2.0',
    'SolidWorks 2024',
    '' );
FILE_SCHEMA (( 'AUTOMOTIVE_DESIGN' ));
ENDSEC;

DATA;
#15=ORIENTED_EDGE ( 'NONE', *, *, #31298, .F. ) ;
#24=ADVANCED_FACE ( 'NONE', ( #40477 ), #35210, .T. ) ;
#32=PLANE ( 'NONE',  #30520 ) ;
#43=ORIENTED_EDGE ( 'NONE', *, *, #31016, .F. ) ;
#88=DIRECTION ( 'NONE',  ( 1.000000000000000000, 0.000000000000000000, 0.000000000000000000 ) ) ;
#95=LINE ( 'NONE', #12201, #34463 ) ;
#117=AXIS2_PLACEMENT_3D ( 'NONE', #32026, #16389, #31621 ) ;
#119=VECTOR ( 'NONE', #8950, 39.37007874015748143 ) ;
#125=CIRCLE ( 'NONE', #26384, 0.1000000000000000194 ) ;
#127=ORIENTED_EDGE ( 'NONE', *, *, #21048, .F. ) ;
#146=DIRECTION ( 'NONE',  ( 0.000000000000000000, 0.000000000000000000, 1.000000000000000000 ) ) ;
#152=VECTOR ( 'NONE', #11344, 39.37007874015748854 ) ;
#157=VECTOR ( 'NONE', #34614, 39.37007874015748143 ) ;
#161=DIRECTION ( 'NONE',  ( -1.000000000000000000, -0.000000000000000000, -0.000000000000000000 ) ) ;
#163=DIRECTION ( 'NONE',  ( -1.000000000000000000, -0.000000000000000000, -0.000000000000000000 ) ) ;
#164=VECTOR ( 'NONE', #40560, 39.37007874015748143 ) ;
#177=EDGE_CURVE ( 'NONE', #19587, #15800, #10226, .T. ) ;
#205=DIRECTION ( 'NONE',  ( 1.000000000000000000, -0.000000000000000000, -0.000000000000000000 ) ) ;
#233=CARTESIAN_POINT ( 'NONE',  ( -0.2746410161513782033, -1.835749455202394298, -0.2938319975228648739 ) ) ;
#244=DIRECTION ( 'NONE',  ( 0.000000000000000000, 0.000000000000000000, -1.000000000000000000 ) ) ;
#250=EDGE_LOOP ( 'NONE', ( #22940, #10850, #32575, #22840 ) ) ;
#259=DIRECTION ( 'NONE',  ( 0.000000000000000000, 0.000000000000000000, -1.000000000000000000 ) ) ;
#267=DIRECTION ( 'NONE',  ( 0.000000000000000000, 0.000000000000000000, 1.000000000000000000 ) ) ;
#268=AXIS2_PLACEMENT_3D ( 'NONE', #15055, #5784, #18341 ) ;
#280=CARTESIAN_POINT ( 'NONE',  ( -0.3000000000000000999, -4.289222312108804225, -0.5708809693675255259 ) ) ;
#284=CARTESIAN_POINT ( 'NONE',  ( -0.3000000000000000999, -2.457388234162025675, -0.5792354969483111127 ) ) ;
#309=ORIENTED_EDGE ( 'NONE', *, *, #24920, .F. ) ;
#319=VECTOR ( 'NONE', #8754, 39.37007874015748854 ) ;
#320=DIRECTION ( 'NONE',  ( 0.000000000000000000, 0.8159412518334724362, 0.5781348229923756188 ) ) ;
#324=( CONVERSION_BASED_UNIT ( 'INCH', #19000 ) LENGTH_UNIT ( ) NAMED_UNIT ( #4430 ) );
#327=CARTESIAN_POINT ( 'NONE',  ( -0.2746410161513776482, -3.941790907013290823, -0.009415996779116623042 ) ) ;
#332=VECTOR ( 'NONE', #28229, 39.37007874015748143 ) ;
#336=AXIS2_PLACEMENT_3D ( 'NONE', #23789, #35713, #20491 ) ;
#345=EDGE_LOOP ( 'NONE', ( #25760, #18511, #17241, #27769 ) ) ;
#352=CARTESIAN_POINT ( 'NONE',  ( -0.2399999999999999079, -1.804235510932644004, -0.1501860188971498311 ) ) ;
#354=VERTEX_POINT ( 'NONE', #32817 ) ;
#355=CARTESIAN_POINT ( 'NONE',  ( -0.2399999999999999079, -1.739646749720735741, -0.3661865639197241507 ) ) ;
#361=CYLINDRICAL_SURFACE ( 'NONE', #26001, 0.06250000000000001388 ) ;
#369=DIRECTION ( 'NONE',  ( 0.000000000000000000, 0.000000000000000000, 1.000000000000000000 ) ) ;
#379=LINE ( 'NONE', #28716, #2161 ) ;
#466=VECTOR ( 'NONE', #25583, 39.37007874015748854 ) ;
#467=ORIENTED_EDGE ( 'NONE', *, *, #19807, .T. ) ;
#473=CARTESIAN_POINT ( 'NONE',  ( -0.2399999999999999079, -2.427691829037316396, -0.9241619397096791921 ) ) ;
#478=VERTEX_POINT ( 'NONE', #40208 ) ;
#480=CIRCLE ( 'NONE', #25394, 0.4615209409081865166 ) ;
#485=CYLINDRICAL_SURFACE ( 'NONE', #13922, 0.1000000000000000194 ) ;
#487=CARTESIAN_POINT ( 'NONE',  ( -0.2399999999999999079, -2.718308734057149678, -0.5229705402004846126 ) ) ;
#526=CARTESIAN_POINT ( 'NONE',  ( -0.2746410161513779258, -3.705001275441084818, -0.3950781284944322458 ) ) ;
#535=ADVANCED_FACE ( 'NONE', ( #35824 ), #9561, .F. ) ;
#547=CARTESIAN_POINT ( 'NONE',  ( -0.2746410161513779258, -3.291368864184587739, -0.6988176298300774469 ) ) ;
#564=ORIENTED_EDGE ( 'NONE', *, *, #37908, .F. ) ;
#591=VERTEX_POINT ( 'NONE', #28693 ) ;
#596=ORIENTED_EDGE ( 'NONE', *, *, #21802, .F. ) ;
#608=ORIENTED_EDGE ( 'NONE', *, *, #35307, .F. ) ;
#620=FACE_BOUND ( 'NONE', #11288, .T. ) ;
#630=DIRECTION ( 'NONE',  ( 1.000000000000000000, -0.000000000000000000, -0.000000000000000000 ) ) ;
#647=LINE ( 'NONE', #13136, #19124 ) ;
#651=ORIENTED_EDGE ( 'NONE', *, *, #25142, .T. ) ;
#654=ADVANCED_FACE ( 'NONE', ( #34847 ), #18926, .T. ) ;
#661=EDGE_CURVE ( 'NONE', #11375, #1766, #37947, .T. ) ;
#665=ORIENTED_EDGE ( 'NONE', *, *, #11458, .F. ) ;
#673=CARTESIAN_POINT ( 'NONE',  ( -0.2399999999999999079, -3.555454838273126139, -0.1971986823720165982 ) ) ;
#676=EDGE_CURVE ( 'NONE', #19999, #32724, #28478, .T. ) ;
#689=CARTESIAN_POINT ( 'NONE',  ( -0.2399999999999999079, -3.952397508731088749, -0.4603303359695052888 ) ) ;
#692=LINE ( 'NONE', #25755, #31554 ) ;
#700=ORIENTED_EDGE ( 'NONE', *, *, #14172, .F. ) ;
#706=ADVANCED_FACE ( 'NONE', ( #10944 ), #34677, .T. ) ;
#726=DIRECTION ( 'NONE',  ( -1.000000000000000000, -0.000000000000000000, -0.000000000000000000 ) ) ;
#731=FACE_OUTER_BOUND ( 'NONE', #20393, .T. ) ;
#774=CYLINDRICAL_SURFACE ( 'NONE', #27850, 0.1000000000000000194 ) ;
#783=VECTOR ( 'NONE', #35125, 39.37007874015748143 ) ;
#792=PLANE ( 'NONE',  #28543 ) ;
#796=CIRCLE ( 'NONE', #23764, 0.1000000000000000194 ) ;
#804=AXIS2_PLACEMENT_3D ( 'NONE', #15978, #21964, #31217 ) ;
#807=ORIENTED_EDGE ( 'NONE', *, *, #4372, .T. ) ;
#817=DIRECTION ( 'NONE',  ( 0.000000000000000000, 0.000000000000000000, -1.000000000000000000 ) ) ;
#825=FACE_OUTER_BOUND ( 'NONE', #10244, .T. ) ;
#839=VERTEX_POINT ( 'NONE', #28601 ) ;
#851=CARTESIAN_POINT ( 'NONE',  ( -0.2399999999999999079, -2.183180860297908144, -0.4937760292030871079 ) ) ;
#855=VECTOR ( 'NONE', #26540, 39.37007874015748143 ) ;
#863=VECTOR ( 'NONE', #31648, 39.37007874015748143 ) ;
#880=LINE ( 'NONE', #19969, #39598 ) ;
#889=AXIS2_PLACEMENT_3D ( 'NONE', #14092, #32801, #28026 ) ;
#902=EDGE_LOOP ( 'NONE', ( #39014, #5058, #6053, #24549 ) ) ;
#910=ORIENTED_EDGE ( 'NONE', *, *, #11433, .T. ) ;
#938=CARTESIAN_POINT ( 'NONE',  ( -0.2399999999999999079, -3.893469231891077520, -0.3535776419057993225 ) ) ;
#946=ORIENTED_EDGE ( 'NONE', *, *, #10762, .T. ) ;
#949=CARTESIAN_POINT ( 'NONE',  ( -0.2746410161513776482, -3.791721498889941255, -0.2726869407194119077 ) ) ;
#950=EDGE_CURVE ( 'NONE', #27945, #16911, #15654, .T. ) ;
#964=ORIENTED_EDGE ( 'NONE', *, *, #36877, .T. ) ;
#968=CARTESIAN_POINT ( 'NONE',  ( -0.2746410161513779258, -3.647187793141847045, -0.4766722536777797115 ) ) ;
#974=CARTESIAN_POINT ( 'NONE',  ( -0.2399999999999999079, -3.899630010830198668, -0.3430483616844877681 ) ) ;
#978=EDGE_LOOP ( 'NONE', ( #32766, #807, #4569, #16901 ) ) ;
#983=AXIS2_PLACEMENT_3D ( 'NONE', #32286, #10909, #29616 ) ;
#1005=CIRCLE ( 'NONE', #38392, 0.1600000000000016964 ) ;
#1032=AXIS2_PLACEMENT_3D ( 'NONE', #1803, #8137, #39223 ) ;
#1039=CARTESIAN_POINT ( 'NONE',  ( -0.2399999999999999079, -2.109195954094405856, -0.3137251058216021793 ) ) ;
#1041=AXIS2_PLACEMENT_3D ( 'NONE', #12619, #5828, #2977 ) ;
#1047=DIRECTION ( 'NONE',  ( 0.4999999999999972800, 0.5006794435238202112, -0.7066258520834632906 ) ) ;
#1049=ORIENTED_EDGE ( 'NONE', *, *, #6247, .T. ) ;
#1056=ORIENTED_EDGE ( 'NONE', *, *, #26817, .F. ) ;
#1066=CIRCLE ( 'NONE', #11535, 0.1000000000000000194 ) ;
#1081=CARTESIAN_POINT ( 'NONE',  ( -0.2399999999999999079, -3.849534981189179028, -0.1910928155360645808 ) ) ;
#1118=CIRCLE ( 'NONE', #36553, 0.5515209409081861525 ) ;
#1126=( CONVERSION_BASED_UNIT ( 'INCH', #10967 ) LENGTH_UNIT ( ) NAMED_UNIT ( #23398 ) );
#1139=CARTESIAN_POINT ( 'NONE',  ( -0.3000000000000000999, -3.941790907013290823, -0.5334369376873030477 ) ) ;
#1141=ORIENTED_EDGE ( 'NONE', *, *, #11510, .T. ) ;
#1142=VECTOR ( 'NONE', #31540, 39.37007874015748854 ) ;
#1148=CARTESIAN_POINT ( 'NONE',  ( -0.3000000000000000999, -3.812085038045152974, -0.02801711824816576976 ) ) ;
#1171=CARTESIAN_POINT ( 'NONE',  ( -0.2746410161513779258, -1.804235510932644004, -0.1501860188971498311 ) ) ;
#1182=CYLINDRICAL_SURFACE ( 'NONE', #40304, 0.1946589359789742957 ) ;
#1191=DIRECTION ( 'NONE',  ( 0.000000000000000000, 0.000000000000000000, -1.000000000000000000 ) ) ;
#1199=VERTEX_POINT ( 'NONE', #30966 ) ;
#1220=CARTESIAN_POINT ( 'NONE',  ( -0.2399999999999999079, -4.289222312108804225, -0.5708809693675255259 ) ) ;
#1222=FACE_OUTER_BOUND ( 'NONE', #3689, .T. ) ;
#1228=CARTESIAN_POINT ( 'NONE',  ( -0.2399999999999999079, -3.985676108854518507, -0.7623095129438225426 ) ) ;
#1229=PLANE ( 'NONE',  #29063 ) ;
#1251=ORIENTED_EDGE ( 'NONE', *, *, #31298, .T. ) ;
#1258=ORIENTED_EDGE ( 'NONE', *, *, #14188, .T. ) ;
#1263=CARTESIAN_POINT ( 'NONE',  ( -0.2399999999999999079, -2.068584980338025847, -0.2731141320652225035 ) ) ;
#1265=CARTESIAN_POINT ( 'NONE',  ( -0.2746410161513779258, -1.730153431576819001, -0.08301574631829765349 ) ) ;
#1268=FACE_OUTER_BOUND ( 'NONE', #19998, .T. ) ;
#1274=DIRECTION ( 'NONE',  ( 1.000000000000000000, -0.000000000000000000, -0.000000000000000000 ) ) ;
#1300=ORIENTED_EDGE ( 'NONE', *, *, #21493, .T. ) ;
#1307=DIRECTION ( 'NONE',  ( -1.000000000000000000, -0.000000000000000000, -0.000000000000000000 ) ) ;
#1326=CARTESIAN_POINT ( 'NONE',  ( -0.2399999999999999079, -1.804235510932644004, -0.1501860188971498311 ) ) ;
#1327=PLANE ( 'NONE',  #30508 ) ;
#1329=CARTESIAN_POINT ( 'NONE',  ( -0.3000000000000000999, -2.289343986263487896, -0.7686455968847020204 ) ) ;
#1347=ORIENTED_EDGE ( 'NONE', *, *, #21802, .T. ) ;
#1370=DIRECTION ( 'NONE',  ( 0.000000000000000000, 0.000000000000000000, 1.000000000000000000 ) ) ;
#1374=ORIENTED_EDGE ( 'NONE', *, *, #23575, .F. ) ;
#1380=CARTESIAN_POINT ( 'NONE',  ( -0.2399999999999999079, -2.511040369707300268, -0.6548468226404909887 ) ) ;
#1392=VERTEX_POINT ( 'NONE', #36270 ) ;
#1395=CARTESIAN_POINT ( 'NONE',  ( -0.2399999999999999079, -2.458279774191353351, -0.8760505995903041798 ) ) ;
#1397=ORIENTED_EDGE ( 'NONE', *, *, #18213, .T. ) ;
#1405=DIRECTION ( 'NONE',  ( 0.000000000000000000, 0.000000000000000000, 1.000000000000000000 ) ) ;
#1414=DIRECTION ( 'NONE',  ( 0.000000000000000000, 0.000000000000000000, -1.000000000000000000 ) ) ;
#1421=DIRECTION ( 'NONE',  ( -1.000000000000000000, 0.000000000000000000, 0.000000000000000000 ) ) ;
#1430=ORIENTED_EDGE ( 'NONE', *, *, #17759, .T. ) ;
#1433=AXIS2_PLACEMENT_3D ( 'NONE', #28038, #88, #40362 ) ;
#1438=LINE ( 'NONE', #17051, #25037 ) ;
#1449=CARTESIAN_POINT ( 'NONE',  ( -0.2399999999999999079, -1.681985126431739364, -0.3495993037578392637 ) ) ;
#1451=DIRECTION ( 'NONE',  ( 0.000000000000000000, 0.000000000000000000, -1.000000000000000000 ) ) ;
#1457=VECTOR ( 'NONE', #15230, 39.37007874015748854 ) ;
#1463=CARTESIAN_POINT ( 'NONE',  ( -0.2746410161513776482, -2.809880844172510272, -0.2480969101616946892 ) ) ;
#1466=CYLINDRICAL_SURFACE ( 'NONE', #40215, 0.1000000000000000194 ) ;
#1472=LINE ( 'NONE', #36411, #11914 ) ;
#1509=LINE ( 'NONE', #32744, #23175 ) ;
#1522=EDGE_CURVE ( 'NONE', #36854, #21617, #12209, .T. ) ;
#1559=CARTESIAN_POINT ( 'NONE',  ( -0.2399999999999999079, -3.286568920421631290, -0.5766864829451954222 ) ) ;
#1568=CARTESIAN_POINT ( 'NONE',  ( -0.2399999999999999079, -3.941790907013290823, -0.4709369376873030477 ) ) ;
#1598=EDGE_LOOP ( 'NONE', ( #11770, #35184, #34446, #21254 ) ) ;
#1638=PLANE ( 'NONE',  #9915 ) ;
#1642=ORIENTED_EDGE ( 'NONE', *, *, #21732, .F. ) ;
#1655=DIRECTION ( 'NONE',  ( 0.000000000000000000, 0.000000000000000000, -1.000000000000000000 ) ) ;
#1666=EDGE_CURVE ( 'NONE', #15505, #9243, #3654, .T. ) ;
#1670=DIRECTION ( 'NONE',  ( 0.000000000000000000, 0.000000000000000000, -1.000000000000000000 ) ) ;
#1704=EDGE_LOOP ( 'NONE', ( #564, #37325, #6115, #12602 ) ) ;
#1716=DIRECTION ( 'NONE',  ( 0.000000000000000000, 0.000000000000000000, -1.000000000000000000 ) ) ;
#1722=CARTESIAN_POINT ( 'NONE',  ( -0.3000000000000000999, -3.672249662662566472, -0.1880352225538197142 ) ) ;
#1727=DIRECTION ( 'NONE',  ( 0.000000000000000000, 3.414809992080317289E-15, -1.000000000000000000 ) ) ;
#1744=CARTESIAN_POINT ( 'NONE',  ( -0.3000000000000000999, -4.134278792318540674, -0.4999285807449073693 ) ) ;
#1766=VERTEX_POINT ( 'NONE', #8142 ) ;
#1768=ADVANCED_FACE ( 'NONE', ( #7314 ), #37523, .T. ) ;
#1775=DIRECTION ( 'NONE',  ( 0.000000000000000000, 0.000000000000000000, -1.000000000000000000 ) ) ;
#1777=CARTESIAN_POINT ( 'NONE',  ( -0.2399999999999999079, -2.853330612949663170, -0.6088139570729240724 ) ) ;
#1781=AXIS2_PLACEMENT_3D ( 'NONE', #3964, #35439, #38321 ) ;
#1786=VERTEX_POINT ( 'NONE', #32826 ) ;
#1789=AXIS2_PLACEMENT_3D ( 'NONE', #39012, #32830, #4255 ) ;
#1800=ORIENTED_EDGE ( 'NONE', *, *, #35811, .F. ) ;
#1803=CARTESIAN_POINT ( 'NONE',  ( -0.3000000000000000999, -2.183180860297908144, -0.4937760292030871079 ) ) ;
#1809=AXIS2_PLACEMENT_3D ( 'NONE', #3737, #19972, #22678 ) ;
#1812=ORIENTED_EDGE ( 'NONE', *, *, #32828, .T. ) ;
#1818=CARTESIAN_POINT ( 'NONE',  ( -0.3000000000000000999, -2.595429044015121534, -0.5484989581857646623 ) ) ;
#1824=DIRECTION ( 'NONE',  ( -1.000000000000000000, 0.000000000000000000, 0.000000000000000000 ) ) ;
#1843=ORIENTED_EDGE ( 'NONE', *, *, #4125, .T. ) ;
#1851=ORIENTED_EDGE ( 'NONE', *, *, #15422, .F. ) ;
#1852=ORIENTED_EDGE ( 'NONE', *, *, #676, .F. ) ;
#1878=EDGE_LOOP ( 'NONE', ( #12193, #13404, #40416, #34916 ) ) ;
#1889=ORIENTED_EDGE ( 'NONE', *, *, #34629, .F. ) ;
#1891=DIRECTION ( 'NONE',  ( 0.4999999999999973910, -0.6123724356957970238, 0.6123724356957940262 ) ) ;
#1895=DIRECTION ( 'NONE',  ( 0.4999999999999973910, 0.000000000000000000, -0.8660254037844402619 ) ) ;
#1907=PLANE ( 'NONE',  #16629 ) ;
#1913=CARTESIAN_POINT ( 'NONE',  ( -0.2399999999999999079, -2.183180860297908144, -0.4937760292030871079 ) ) ;
#1928=FACE_OUTER_BOUND ( 'NONE', #12187, .T. ) ;
#1933=ORIENTED_EDGE ( 'NONE', *, *, #14710, .F. ) ;
#1937=CARTESIAN_POINT ( 'NONE',  ( -0.2399999999999999079, -3.701811653776600597, -0.3192834175180689904 ) ) ;
#1969=ORIENTED_EDGE ( 'NONE', *, *, #14539, .F. ) ;
#1977=DIRECTION ( 'NONE',  ( -1.000000000000000000, -0.000000000000000000, -0.000000000000000000 ) ) ;
#1983=ORIENTED_EDGE ( 'NONE', *, *, #3168, .T. ) ;
#2003=AXIS2_PLACEMENT_3D ( 'NONE', #6309, #19071, #16200 ) ;
#2017=DIRECTION ( 'NONE',  ( 0.000000000000000000, 0.000000000000000000, 1.000000000000000000 ) ) ;
#2019=ORIENTED_EDGE ( 'NONE', *, *, #27363, .F. ) ;
#2037=VECTOR ( 'NONE', #2838, 39.37007874015748854 ) ;
#2038=EDGE_LOOP ( 'NONE', ( #2765, #36816, #4537, #27383 ) ) ;
#2048=DIRECTION ( 'NONE',  ( 1.000000000000000000, -0.000000000000000000, -0.000000000000000000 ) ) ;
#2058=CARTESIAN_POINT ( 'NONE',  ( -0.2746410161513779258, -2.511040369707300268, -0.5948468226404902692 ) ) ;
#2079=ORIENTED_EDGE ( 'NONE', *, *, #4175, .T. ) ;
#2086=DIRECTION ( 'NONE',  ( 0.000000000000000000, 0.000000000000000000, -1.000000000000000000 ) ) ;
#2088=AXIS2_PLACEMENT_3D ( 'NONE', #2924, #2524, #21652 ) ;
#2093=CARTESIAN_POINT ( 'NONE',  ( -0.2746410161513782033, -2.003129936916423048, -0.4197911229995844873 ) ) ;
#2095=LINE ( 'NONE', #1722, #38440 ) ;
#2097=DIRECTION ( 'NONE',  ( -1.000000000000000000, 0.000000000000000000, 0.000000000000000000 ) ) ;
#2106=DIRECTION ( 'NONE',  ( 0.000000000000000000, 0.000000000000000000, -1.000000000000000000 ) ) ;
#2116=CIRCLE ( 'NONE', #20532, 0.6115209409081865388 ) ;
#2130=DIRECTION ( 'NONE',  ( 0.000000000000000000, 0.5365213554527465956, -0.8438867430782092116 ) ) ;
#2153=FACE_OUTER_BOUND ( 'NONE', #21960, .T. ) ;
#2161=VECTOR ( 'NONE', #163, 39.37007874015748143 ) ;
#2164=DIRECTION ( 'NONE',  ( -1.000000000000000000, -0.000000000000000000, -0.000000000000000000 ) ) ;
#2165=FACE_OUTER_BOUND ( 'NONE', #23989, .T. ) ;
#2168=ORIENTED_EDGE ( 'NONE', *, *, #35075, .T. ) ;
#2189=DIRECTION ( 'NONE',  ( 0.000000000000000000, 0.8159412518334721032, 0.5781348229923762849 ) ) ;
#2204=VECTOR ( 'NONE', #7460, 39.37007874015748143 ) ;
#2212=CARTESIAN_POINT ( 'NONE',  ( -0.2399999999999999079, -2.477126460671948749, -0.4732852368073287574 ) ) ;
#2219=AXIS2_PLACEMENT_3D ( 'NONE', #27051, #33220, #30136 ) ;
#2220=DIRECTION ( 'NONE',  ( -1.000000000000000000, 0.000000000000000000, 0.000000000000000000 ) ) ;
#2235=CARTESIAN_POINT ( 'NONE',  ( -0.2746410161513779258, -2.139295658456680904, -0.3024034539465678129 ) ) ;
#2244=CIRCLE ( 'NONE', #10779, 0.1000000000000000194 ) ;
#2247=DIRECTION ( 'NONE',  ( -1.000000000000000000, -0.000000000000000000, -0.000000000000000000 ) ) ;
#2257=EDGE_CURVE ( 'NONE', #10465, #22886, #12955, .T. ) ;
#2282=FACE_OUTER_BOUND ( 'NONE', #31562, .T. ) ;
#2291=DIRECTION ( 'NONE',  ( 1.000000000000000000, -0.000000000000000000, -0.000000000000000000 ) ) ;
#2307=CARTESIAN_POINT ( 'NONE',  ( -0.2399999999999999079, -3.941790907013290823, 0.08058400322088303536 ) ) ;
#2308=AXIS2_PLACEMENT_3D ( 'NONE', #39626, #17628, #1405 ) ;
#2331=CARTESIAN_POINT ( 'NONE',  ( -0.2399999999999999079, -2.375187403135927688, -0.6336237179921873075 ) ) ;
#2334=CONICAL_SURFACE ( 'NONE', #5598, 0.1600000000000000588, 1.047197551196602516 ) ;
#2342=FACE_OUTER_BOUND ( 'NONE', #37522, .T. ) ;
#2349=VERTEX_POINT ( 'NONE', #9469 ) ;
#2351=DIRECTION ( 'NONE',  ( 1.000000000000000000, -0.000000000000000000, -0.000000000000000000 ) ) ;
#2354=DIRECTION ( 'NONE',  ( 0.000000000000000000, 0.000000000000000000, 1.000000000000000000 ) ) ;
#2355=EDGE_CURVE ( 'NONE', #31920, #15882, #33751, .T. ) ;
#2369=ORIENTED_EDGE ( 'NONE', *, *, #23378, .F. ) ;
#2372=CIRCLE ( 'NONE', #15530, 0.1000000000000000194 ) ;
#2411=DIRECTION ( 'NONE',  ( -1.000000000000000000, 0.000000000000000000, 0.000000000000000000 ) ) ;
#2426=DIRECTION ( 'NONE',  ( 0.000000000000000000, 0.000000000000000000, -1.000000000000000000 ) ) ;
#2427=LINE ( 'NONE', #33670, #35050 ) ;
#2432=FACE_OUTER_BOUND ( 'NONE', #29977, .T. ) ;
#2437=DIRECTION ( 'NONE',  ( -0.5000000000000002220, 0.000000000000000000, 0.8660254037844384856 ) ) ;
#2441=ORIENTED_EDGE ( 'NONE', *, *, #16789, .F. ) ;
#2442=EDGE_CURVE ( 'NONE', #19638, #14679, #40364, .T. ) ;
#2447=CARTESIAN_POINT ( 'NONE',  ( -0.2399999999999999079, -4.098813193844367042, -0.6491724279539748954 ) ) ;
#2450=ORIENTED_EDGE ( 'NONE', *, *, #39553, .F. ) ;
#2451=EDGE_LOOP ( 'NONE', ( #36493, #3544, #24242, #1374 ) ) ;
#2467=CARTESIAN_POINT ( 'NONE',  ( -0.2399999999999999079, -3.985676108854518507, -0.7623095129438225426 ) ) ;
#2475=DIRECTION ( 'NONE',  ( 1.000000000000000000, -0.000000000000000000, -0.000000000000000000 ) ) ;
#2481=CARTESIAN_POINT ( 'NONE',  ( -0.2399999999999999079, -3.156018320128275878, -0.4841849112664152743 ) ) ;
#2504=EDGE_CURVE ( 'NONE', #29444, #27585, #33298, .T. ) ;
#2524=DIRECTION ( 'NONE',  ( 1.000000000000000000, -0.000000000000000000, -0.000000000000000000 ) ) ;
#2528=ADVANCED_FACE ( 'NONE', ( #24678 ), #18474, .F. ) ;
#2548=ORIENTED_EDGE ( 'NONE', *, *, #32777, .F. ) ;
#2568=ORIENTED_EDGE ( 'NONE', *, *, #40595, .T. ) ;
#2581=ORIENTED_EDGE ( 'NONE', *, *, #33306, .T. ) ;
#2584=CARTESIAN_POINT ( 'NONE',  ( -0.2399999999999999079, -2.183180860297908144, -0.4937760292030871079 ) ) ;
#2610=LINE ( 'NONE', #34682, #17969 ) ;
#2613=DIRECTION ( 'NONE',  ( -1.000000000000000000, -0.000000000000000000, -0.000000000000000000 ) ) ;
#2614=LINE ( 'NONE', #15575, #22565 ) ;
#2621=VERTEX_POINT ( 'NONE', #9823 ) ;
#2625=DIRECTION ( 'NONE',  ( -1.000000000000000000, -0.000000000000000000, -0.000000000000000000 ) ) ;
#2632=ORIENTED_EDGE ( 'NONE', *, *, #17439, .T. ) ;
#2660=EDGE_CURVE ( 'NONE', #11781, #10668, #11478, .T. ) ;
#2670=CIRCLE ( 'NONE', #8556, 0.5215209409081880132 ) ;
#2671=EDGE_CURVE ( 'NONE', #31622, #14323, #1005, .T. ) ;
#2675=VECTOR ( 'NONE', #14935, 39.37007874015748143 ) ;
#2706=EDGE_CURVE ( 'NONE', #4081, #38935, #5529, .T. ) ;
#2713=DIRECTION ( 'NONE',  ( 0.000000000000000000, 0.9343694307158671997, -0.3563057211773426602 ) ) ;
#2721=CIRCLE ( 'NONE', #18488, 0.1946589359789743512 ) ;
#2727=ORIENTED_EDGE ( 'NONE', *, *, #7131, .T. ) ;
#2730=CONICAL_SURFACE ( 'NONE', #23767, 0.5515209409081860414, 1.047197551196597409 ) ;
#2735=EDGE_LOOP ( 'NONE', ( #13647, #1933, #16103, #29692 ) ) ;
#2752=LINE ( 'NONE', #15302, #31810 ) ;
#2765=ORIENTED_EDGE ( 'NONE', *, *, #7608, .T. ) ;
#2779=DIRECTION ( 'NONE',  ( 0.000000000000000000, 0.000000000000000000, -1.000000000000000000 ) ) ;
#2784=ORIENTED_EDGE ( 'NONE', *, *, #22552, .F. ) ;
#2786=VERTEX_POINT ( 'NONE', #39622 ) ;
#2796=CARTESIAN_POINT ( 'NONE',  ( -0.2399999999999999079, -2.139295658456680904, -0.2024034539465678073 ) ) ;
#2817=EDGE_LOOP ( 'NONE', ( #37631, #37371, #35607, #37980 ) ) ;
#2821=VECTOR ( 'NONE', #21632, 39.37007874015748143 ) ;
#2838=DIRECTION ( 'NONE',  ( 0.5000000000000019984, 0.4646411234949395785, -0.7308273574226392677 ) ) ;
#2857=DIRECTION ( 'NONE',  ( -1.000000000000000000, -0.000000000000000000, -0.000000000000000000 ) ) ;
#2870=DIRECTION ( 'NONE',  ( 1.000000000000000000, 0.000000000000000000, 0.000000000000000000 ) ) ;
#2883=AXIS2_PLACEMENT_3D ( 'NONE', #27376, #39901, #24281 ) ;
#2887=ORIENTED_EDGE ( 'NONE', *, *, #35863, .F. ) ;
#2924=CARTESIAN_POINT ( 'NONE',  ( -0.2746410161513782033, -2.289343986263487896, -0.7686455968847020204 ) ) ;
#2926=FACE_OUTER_BOUND ( 'NONE', #23944, .T. ) ;
#2944=DIRECTION ( 'NONE',  ( 1.000000000000000000, 0.000000000000000000, 0.000000000000000000 ) ) ;
#2953=EDGE_CURVE ( 'NONE', #10668, #11891, #27307, .T. ) ;
#2961=DIRECTION ( 'NONE',  ( 0.000000000000000000, 0.000000000000000000, 1.000000000000000000 ) ) ;
#2977=DIRECTION ( 'NONE',  ( 0.000000000000000000, 0.000000000000000000, -1.000000000000000000 ) ) ;
#2985=CARTESIAN_POINT ( 'NONE',  ( -0.2746410161513779258, -2.183180860297908144, -0.4937760292030871079 ) ) ;
#3011=CIRCLE ( 'NONE', #27971, 0.1346589359789736318 ) ;
#3018=DIRECTION ( 'NONE',  ( 0.4999999999999998890, 0.3297230132044474127, 0.8008013077932500945 ) ) ;
#3024=AXIS2_PLACEMENT_3D ( 'NONE', #15931, #14007, #12632 ) ;
#3026=CIRCLE ( 'NONE', #8915, 0.1000000000000000194 ) ;
#3032=ORIENTED_EDGE ( 'NONE', *, *, #37288, .T. ) ;
#3033=CARTESIAN_POINT ( 'NONE',  ( -0.2399999999999999079, -4.015775813216793999, -0.6509878610687880318 ) ) ;
#3052=ORIENTED_EDGE ( 'NONE', *, *, #22552, .T. ) ;
#3055=DIRECTION ( 'NONE',  ( -0.4999999999999998890, 0.6123724356957955806, -0.6123724356957935822 ) ) ;
#3061=AXIS2_PLACEMENT_3D ( 'NONE', #39665, #5291, #18467 ) ;
#3086=EDGE_LOOP ( 'NONE', ( #7463, #3834, #34389, #25369 ) ) ;
#3125=DIRECTION ( 'NONE',  ( -1.000000000000000000, -0.000000000000000000, -0.000000000000000000 ) ) ;
#3126=EDGE_CURVE ( 'NONE', #33134, #25252, #39747, .T. ) ;
#3141=EDGE_CURVE ( 'NONE', #14090, #7026, #14797, .T. ) ;
#3165=VERTEX_POINT ( 'NONE', #10799 ) ;
#3168=EDGE_CURVE ( 'NONE', #15800, #36123, #18051, .T. ) ;
#3177=ORIENTED_EDGE ( 'NONE', *, *, #2504, .F. ) ;
#3179=DIRECTION ( 'NONE',  ( 0.000000000000000000, 1.786920323354501031E-15, -1.000000000000000000 ) ) ;
#3188=ORIENTED_EDGE ( 'NONE', *, *, #6625, .F. ) ;
#3201=DIRECTION ( 'NONE',  ( 0.000000000000000000, 0.000000000000000000, -1.000000000000000000 ) ) ;
#3220=DIRECTION ( 'NONE',  ( 0.000000000000000000, 0.000000000000000000, -1.000000000000000000 ) ) ;
#3226=CARTESIAN_POINT ( 'NONE',  ( -0.2399999999999999079, -3.068736697824635318, 0.08412833800243585403 ) ) ;
#3241=ORIENTED_EDGE ( 'NONE', *, *, #13667, .T. ) ;
#3250=FACE_BOUND ( 'NONE', #26826, .T. ) ;
#3273=CARTESIAN_POINT ( 'NONE',  ( -0.2399999999999999079, -2.183180860297908144, -0.4937760292030871079 ) ) ;
#3280=ORIENTED_EDGE ( 'NONE', *, *, #12547, .F. ) ;
#3300=DIRECTION ( 'NONE',  ( -1.000000000000000000, -0.000000000000000000, -0.000000000000000000 ) ) ;
#3317=VERTEX_POINT ( 'NONE', #36698 ) ;
#3326=ORIENTED_EDGE ( 'NONE', *, *, #40406, .F. ) ;
#3327=ADVANCED_FACE ( 'NONE', ( #8506 ), #36462, .T. ) ;
#3337=VECTOR ( 'NONE', #6874, 39.37007874015748854 ) ;
#3364=FACE_OUTER_BOUND ( 'NONE', #27165, .T. ) ;
#3381=ORIENTED_EDGE ( 'NONE', *, *, #18262, .T. ) ;
#3383=ORIENTED_EDGE ( 'NONE', *, *, #31153, .F. ) ;
#3394=CYLINDRICAL_SURFACE ( 'NONE', #8812, 0.06250000000000001388 ) ;
#3399=AXIS2_PLACEMENT_3D ( 'NONE', #5164, #11350, #40130 ) ;
#3410=DIRECTION ( 'NONE',  ( 0.000000000000000000, 0.000000000000000000, -1.000000000000000000 ) ) ;
#3415=CARTESIAN_POINT ( 'NONE',  ( -0.2399999999999999079, -1.832519782180105805, -0.1219017476496882246 ) ) ;
#3475=LINE ( 'NONE', #25293, #11386 ) ;
#3514=CARTESIAN_POINT ( 'NONE',  ( -0.2399999999999999079, -3.757033409510397881, -0.3216434158294207424 ) ) ;
#3516=LINE ( 'NONE', #9077, #32287 ) ;
#3518=AXIS2_PLACEMENT_3D ( 'NONE', #1329, #13836, #32764 ) ;
#3535=ORIENTED_EDGE ( 'NONE', *, *, #4922, .F. ) ;
#3538=DIRECTION ( 'NONE',  ( -1.000000000000000000, -0.000000000000000000, -0.000000000000000000 ) ) ;
#3544=ORIENTED_EDGE ( 'NONE', *, *, #4505, .T. ) ;
#3546=VECTOR ( 'NONE', #24189, 39.37007874015748143 ) ;
#3556=AXIS2_PLACEMENT_3D ( 'NONE', #35780, #33868, #39272 ) ;
#3559=CIRCLE ( 'NONE', #23285, 0.1600000000000007527 ) ;
#3561=( LENGTH_UNIT ( ) NAMED_UNIT ( * ) SI_UNIT ( $, .METRE. ) );
#3582=ORIENTED_EDGE ( 'NONE', *, *, #4913, .F. ) ;
#3585=CIRCLE ( 'NONE', #26603, 0.5215209409081871250 ) ;
#3599=EDGE_CURVE ( 'NONE', #35563, #23695, #18996, .T. ) ;
#3606=CARTESIAN_POINT ( 'NONE',  ( -0.2399999999999999079, -3.941790907013290823, -0.4709369376873030477 ) ) ;
#3619=DIRECTION ( 'NONE',  ( 0.000000000000000000, 0.000000000000000000, 1.000000000000000000 ) ) ;
#3621=EDGE_CURVE ( 'NONE', #27741, #9411, #28446, .T. ) ;
#3640=DIRECTION ( 'NONE',  ( 1.000000000000000000, -0.000000000000000000, -0.000000000000000000 ) ) ;
#3654=LINE ( 'NONE', #28336, #783 ) ;
#3666=CARTESIAN_POINT ( 'NONE',  ( -0.3000000000000000999, -3.253611865733782693, -0.3464478357516359575 ) ) ;
#3677=CARTESIAN_POINT ( 'NONE',  ( -0.3000000000000000999, -3.753843787845913216, -0.2458487048530572650 ) ) ;
#3681=ADVANCED_FACE ( 'NONE', ( #16721 ), #4153, .F. ) ;
#3685=CARTESIAN_POINT ( 'NONE',  ( -0.2399999999999999079, -2.853330612949663170, -0.6088139570729240724 ) ) ;
#3689=EDGE_LOOP ( 'NONE', ( #36122, #15778, #15173, #18265 ) ) ;
#3695=DIRECTION ( 'NONE',  ( 1.000000000000000000, -0.000000000000000000, -0.000000000000000000 ) ) ;
#3723=CARTESIAN_POINT ( 'NONE',  ( -0.3000000000000000999, -2.253314830856113726, -0.6753616220517687507 ) ) ;
#3727=AXIS2_PLACEMENT_3D ( 'NONE', #27001, #11767, #2106 ) ;
#3737=CARTESIAN_POINT ( 'NONE',  ( -0.2746410161513779258, -3.941790907013290823, -0.4709369376873030477 ) ) ;
#3744=DIRECTION ( 'NONE',  ( 0.000000000000000000, 0.000000000000000000, -1.000000000000000000 ) ) ;
#3757=AXIS2_PLACEMENT_3D ( 'NONE', #18548, #3125, #12183 ) ;
#3771=CARTESIAN_POINT ( 'NONE',  ( -0.2399999999999999079, -2.477126460671948749, -0.4732852368073287574 ) ) ;
#3776=ADVANCED_FACE ( 'NONE', ( #15803 ), #8259, .T. ) ;
#3785=VECTOR ( 'NONE', #10516, 39.37007874015748143 ) ;
#3813=CARTESIAN_POINT ( 'NONE',  ( -0.2399999999999999079, -3.609310082097819894, -0.4498340178114252352 ) ) ;
#3821=DIRECTION ( 'NONE',  ( 1.000000000000000000, -0.000000000000000000, -0.000000000000000000 ) ) ;
#3829=CARTESIAN_POINT ( 'NONE',  ( -0.2399999999999999079, -2.050023788963422078, -0.4737205214156571809 ) ) ;
#3832=ORIENTED_EDGE ( 'NONE', *, *, #6625, .T. ) ;
#3834=ORIENTED_EDGE ( 'NONE', *, *, #9692, .T. ) ;
#3847=CARTESIAN_POINT ( 'NONE',  ( -0.2399999999999999079, -2.292669950144801572, -0.8383185228372386222 ) ) ;
#3848=EDGE_CURVE ( 'NONE', #24392, #11781, #14140, .T. ) ;
#3861=CARTESIAN_POINT ( 'NONE',  ( -0.2399999999999999079, -1.990692974992658737, -0.4647843861454829528 ) ) ;
#3866=FACE_OUTER_BOUND ( 'NONE', #18501, .T. ) ;
#3897=CARTESIAN_POINT ( 'NONE',  ( -0.3000000000000000999, -3.753843787845913216, -0.2458487048530572372 ) ) ;
#3900=EDGE_CURVE ( 'NONE', #33422, #25941, #20741, .T. ) ;
#3903=DIRECTION ( 'NONE',  ( -1.000000000000000000, -0.000000000000000000, -0.000000000000000000 ) ) ;
#3919=DIRECTION ( 'NONE',  ( 0.000000000000000000, 0.7071067811865475727, -0.7071067811865475727 ) ) ;
#3932=CARTESIAN_POINT ( 'NONE',  ( -0.2746410161513770931, -2.853330612949663170, -0.6088139570729240724 ) ) ;
#3941=ORIENTED_EDGE ( 'NONE', *, *, #4230, .T. ) ;
#3964=CARTESIAN_POINT ( 'NONE',  ( -0.2399999999999999079, -2.183180860297908144, -0.4937760292030871079 ) ) ;
#3967=DIRECTION ( 'NONE',  ( 0.000000000000000000, -0.9246857012436752177, 0.3807313408632029827 ) ) ;
#3978=ORIENTED_EDGE ( 'NONE', *, *, #39551, .F. ) ;
#3993=EDGE_CURVE ( 'NONE', #32724, #6555, #20123, .T. ) ;
#3998=CARTESIAN_POINT ( 'NONE',  ( -0.2746410161513779258, -2.595429044015121534, -0.5484989581857646623 ) ) ;
#4014=PLANE ( 'NONE',  #33177 ) ;
#4019=ORIENTED_EDGE ( 'NONE', *, *, #6733, .T. ) ;
#4031=DIRECTION ( 'NONE',  ( -1.000000000000000000, -0.000000000000000000, -0.000000000000000000 ) ) ;
#4033=AXIS2_PLACEMENT_3D ( 'NONE', #25608, #38138, #35057 ) ;
#4038=ORIENTED_EDGE ( 'NONE', *, *, #2504, .T. ) ;
#4039=CONICAL_SURFACE ( 'NONE', #24440, 0.1600000000000018352, 1.047197551196601850 ) ;
#4067=CONICAL_SURFACE ( 'NONE', #38259, 0.1600000000000006140, 1.047197551196598075 ) ;
#4071=ORIENTED_EDGE ( 'NONE', *, *, #29129, .T. ) ;
#4072=EDGE_LOOP ( 'NONE', ( #6658, #16104, #5131, #30998 ) ) ;
#4081=VERTEX_POINT ( 'NONE', #10857 ) ;
#4088=AXIS2_PLACEMENT_3D ( 'NONE', #27597, #24520, #23706 ) ;
#4120=ORIENTED_EDGE ( 'NONE', *, *, #8917, .T. ) ;
#4123=FACE_OUTER_BOUND ( 'NONE', #12694, .T. ) ;
#4124=CONICAL_SURFACE ( 'NONE', #35584, 0.1600000000000006972, 1.047197551196600074 ) ;
#4125=EDGE_CURVE ( 'NONE', #32592, #6266, #26705, .T. ) ;
#4130=VERTEX_POINT ( 'NONE', #18425 ) ;
#4150=AXIS2_PLACEMENT_3D ( 'NONE', #39470, #5300, #4912 ) ;
#4153=PLANE ( 'NONE',  #31893 ) ;
#4154=AXIS2_PLACEMENT_3D ( 'NONE', #34275, #28122, #12666 ) ;
#4175=EDGE_CURVE ( 'NONE', #38034, #29444, #24034, .T. ) ;
#4190=ORIENTED_EDGE ( 'NONE', *, *, #13996, .T. ) ;
#4201=ORIENTED_EDGE ( 'NONE', *, *, #31153, .T. ) ;
#4213=VECTOR ( 'NONE', #30339, 39.37007874015748143 ) ;
#4230=EDGE_CURVE ( 'NONE', #17567, #4836, #18238, .T. ) ;
#4232=EDGE_LOOP ( 'NONE', ( #29581, #27118, #25314, #28340 ) ) ;
#4241=CARTESIAN_POINT ( 'NONE',  ( -0.2399999999999999079, -3.941790907013290823, -0.4709369376873030477 ) ) ;
#4255=DIRECTION ( 'NONE',  ( 0.000000000000000000, 0.000000000000000000, -1.000000000000000000 ) ) ;
#4257=ORIENTED_EDGE ( 'NONE', *, *, #7205, .F. ) ;
#4266=CARTESIAN_POINT ( 'NONE',  ( -0.2399999999999999079, -2.393162167644017568, -1.003759557197344554 ) ) ;
#4268=CARTESIAN_POINT ( 'NONE',  ( -0.2399999999999999079, -4.320736256378554963, -0.8145269479932405465 ) ) ;
#4296=ORIENTED_EDGE ( 'NONE', *, *, #38099, .F. ) ;
#4307=PLANE ( 'NONE',  #29003 ) ;
#4310=CARTESIAN_POINT ( 'NONE',  ( -0.3000000000000000999, -2.511040369707300268, -0.4948468226404901804 ) ) ;
#4328=LINE ( 'NONE', #17676, #31781 ) ;
#4334=ORIENTED_EDGE ( 'NONE', *, *, #32557, .T. ) ;
#4336=DIRECTION ( 'NONE',  ( 0.000000000000000000, 0.000000000000000000, -1.000000000000000000 ) ) ;
#4343=DIRECTION ( 'NONE',  ( -1.000000000000000000, -0.000000000000000000, -0.000000000000000000 ) ) ;
#4346=DIRECTION ( 'NONE',  ( -1.000000000000000000, 0.000000000000000000, 0.000000000000000000 ) ) ;
#4358=CYLINDRICAL_SURFACE ( 'NONE', #27162, 0.1946589359789742957 ) ;
#4361=VECTOR ( 'NONE', #24036, 39.37007874015748143 ) ;
#4372=EDGE_CURVE ( 'NONE', #27821, #20248, #29278, .T. ) ;
#4389=ORIENTED_EDGE ( 'NONE', *, *, #17255, .F. ) ;
#4414=ADVANCED_FACE ( 'NONE', ( #29108 ), #10198, .T. ) ;
#4430=DIMENSIONAL_EXPONENTS ( 1.000000000000000000, 0.000000000000000000, 0.000000000000000000, 0.000000000000000000, 0.000000000000000000, 0.000000000000000000, 0.000000000000000000 ) ;
#4448=ORIENTED_EDGE ( 'NONE', *, *, #31016, .T. ) ;
#4449=LINE ( 'NONE', #4636, #35273 ) ;
#4505=EDGE_CURVE ( 'NONE', #36967, #11216, #35878, .T. ) ;
#4516=DIRECTION ( 'NONE',  ( 0.000000000000000000, 0.5781348229923758408, -0.8159412518334724362 ) ) ;
#4528=EDGE_LOOP ( 'NONE', ( #4727, #38829, #31927, #17856 ) ) ;
#4534=DIRECTION ( 'NONE',  ( 1.000000000000000000, 0.000000000000000000, 0.000000000000000000 ) ) ;
#4537=ORIENTED_EDGE ( 'NONE', *, *, #5199, .F. ) ;
#4545=CARTESIAN_POINT ( 'NONE',  ( -0.3000000000000000999, -2.845511416290244622, -0.3415338532332813926 ) ) ;
#4549=CARTESIAN_POINT ( 'NONE',  ( -0.3000000000000000999, -2.183180860297908144, -0.4937760292030871079 ) ) ;
#4564=DIRECTION ( 'NONE',  ( -0.4261641068392694742, -0.9046458721742379749, 0.000000000000000000 ) ) ;
#4569=ORIENTED_EDGE ( 'NONE', *, *, #20237, .F. ) ;
#4574=CARTESIAN_POINT ( 'NONE',  ( -0.2746410161513779258, -3.941790907013290823, -0.4709369376873030477 ) ) ;
#4576=DIRECTION ( 'NONE',  ( 0.000000000000000000, 0.000000000000000000, 1.000000000000000000 ) ) ;
#4577=EDGE_LOOP ( 'NONE', ( #19787, #4718, #24103, #39699 ) ) ;
#4594=DIRECTION ( 'NONE',  ( 0.000000000000000000, 8.195543980992787683E-15, -1.000000000000000000 ) ) ;
#4604=AXIS2_PLACEMENT_3D ( 'NONE', #2481, #8843, #244 ) ;
#4626=DIRECTION ( 'NONE',  ( 0.000000000000000000, 0.7071067811865465735, 0.7071067811865484609 ) ) ;
#4635=VERTEX_POINT ( 'NONE', #1559 ) ;
#4636=CARTESIAN_POINT ( 'NONE',  ( -0.2399999999999999079, -3.745280840418592661, 0.04438736989695814261 ) ) ;
#4660=VECTOR ( 'NONE', #6104, 39.37007874015748143 ) ;
#4663=AXIS2_PLACEMENT_3D ( 'NONE', #23891, #33517, #36420 ) ;
#4696=CARTESIAN_POINT ( 'NONE',  ( -0.3000000000000000999, -1.835749455202394298, -0.3938319975228649072 ) ) ;
#4703=DIRECTION ( 'NONE',  ( -1.000000000000000000, -0.000000000000000000, -0.000000000000000000 ) ) ;
#4705=AXIS2_PLACEMENT_3D ( 'NONE', #1777, #35472, #17587 ) ;
#4707=DIRECTION ( 'NONE',  ( 1.000000000000000000, 0.000000000000000000, 0.000000000000000000 ) ) ;
#4709=CIRCLE ( 'NONE', #804, 0.03999999999999933470 ) ;
#4718=ORIENTED_EDGE ( 'NONE', *, *, #30275, .F. ) ;
#4727=ORIENTED_EDGE ( 'NONE', *, *, #28356, .T. ) ;
#4744=DIRECTION ( 'NONE',  ( 0.000000000000000000, 0.000000000000000000, -1.000000000000000000 ) ) ;
#4750=FACE_BOUND ( 'NONE', #27004, .T. ) ;
#4765=CARTESIAN_POINT ( 'NONE',  ( -0.2746410161513782033, -2.461298705151934829, -0.7594706439553173816 ) ) ;
#4789=AXIS2_PLACEMENT_3D ( 'NONE', #8567, #5272, #40042 ) ;
#4812=DIRECTION ( 'NONE',  ( -1.000000000000000000, -0.000000000000000000, -0.000000000000000000 ) ) ;
#4819=MANIFOLD_SOLID_BREP ( 'Chamfer1', #31915 ) ;
#4836=VERTEX_POINT ( 'NONE', #33408 ) ;
#4842=ORIENTED_EDGE ( 'NONE', *, *, #37818, .T. ) ;
#4847=CARTESIAN_POINT ( 'NONE',  ( -0.2746410161513782033, -2.407646569606659792, -0.8438593182631384249 ) ) ;
#4857=AXIS2_PLACEMENT_3D ( 'NONE', #2796, #29815, #1655 ) ;
#4860=AXIS2_PLACEMENT_3D ( 'NONE', #26335, #17272, #13973 ) ;
#4862=DIRECTION ( 'NONE',  ( 0.000000000000000000, 0.000000000000000000, -1.000000000000000000 ) ) ;
#4863=ADVANCED_FACE ( 'NONE', ( #2153 ), #36701, .T. ) ;
#4876=AXIS2_PLACEMENT_3D ( 'NONE', #40067, #11896, #33928 ) ;
#4877=ORIENTED_EDGE ( 'NONE', *, *, #21085, .T. ) ;
#4880=DIRECTION ( 'NONE',  ( 1.000000000000000000, 0.000000000000000000, 0.000000000000000000 ) ) ;
#4884=VERTEX_POINT ( 'NONE', #16130 ) ;
#4894=DIRECTION ( 'NONE',  ( 0.000000000000000000, 0.000000000000000000, 1.000000000000000000 ) ) ;
#4905=DIRECTION ( 'NONE',  ( 1.000000000000000000, 0.000000000000000000, 0.000000000000000000 ) ) ;
#4908=VECTOR ( 'NONE', #2189, 39.37007874015748854 ) ;
#4912=DIRECTION ( 'NONE',  ( 0.000000000000000000, 0.000000000000000000, 1.000000000000000000 ) ) ;
#4913=EDGE_CURVE ( 'NONE', #12108, #11891, #3026, .T. ) ;
#4914=CARTESIAN_POINT ( 'NONE',  ( -0.3000000000000000999, -3.941790907013290823, -0.4709369376873030477 ) ) ;
#4916=DIRECTION ( 'NONE',  ( -1.000000000000000000, 0.000000000000000000, 0.000000000000000000 ) ) ;
#4922=EDGE_CURVE ( 'NONE', #24814, #26475, #28247, .T. ) ;
#4935=CARTESIAN_POINT ( 'NONE',  ( -0.2399999999999999079, -3.061672939615505573, -1.351054905085088409 ) ) ;
#4942=EDGE_LOOP ( 'NONE', ( #14318, #27837, #27032, #28634 ) ) ;
#4946=CARTESIAN_POINT ( 'NONE',  ( -0.2746410161513782033, -1.906460133321048911, -0.3231213194042100723 ) ) ;
#4955=AXIS2_PLACEMENT_3D ( 'NONE', #7603, #35586, #10093 ) ;
#4995=EDGE_CURVE ( 'NONE', #591, #36967, #23526, .T. ) ;
#4996=CARTESIAN_POINT ( 'NONE',  ( -0.2399999999999999079, -3.985676108854518507, -0.7623095129438225426 ) ) ;
#5026=CIRCLE ( 'NONE', #3727, 0.6115209409081865388 ) ;
#5028=ORIENTED_EDGE ( 'NONE', *, *, #11433, .F. ) ;
#5034=ORIENTED_EDGE ( 'NONE', *, *, #950, .F. ) ;
#5052=DIRECTION ( 'NONE',  ( -1.000000000000000000, -0.000000000000000000, -0.000000000000000000 ) ) ;
#5058=ORIENTED_EDGE ( 'NONE', *, *, #35119, .T. ) ;
#5086=DIRECTION ( 'NONE',  ( 0.000000000000000000, -0.5781348229923757298, 0.8159412518334727693 ) ) ;
#5103=ORIENTED_EDGE ( 'NONE', *, *, #37614, .T. ) ;
#5106=CARTESIAN_POINT ( 'NONE',  ( -0.2399999999999999079, -3.723902497147952406, 0.1004495357399106253 ) ) ;
#5127=CARTESIAN_POINT ( 'NONE',  ( -0.2746410161513776482, -3.812085038045152974, -0.02801711824816583915 ) ) ;
#5131=ORIENTED_EDGE ( 'NONE', *, *, #2953, .F. ) ;
#5132=DIRECTION ( 'NONE',  ( 0.3779644730092284743, 0.9258200997725509751, 0.000000000000000000 ) ) ;
#5133=PLANE ( 'NONE',  #4663 ) ;
#5141=ORIENTED_EDGE ( 'NONE', *, *, #24940, .F. ) ;
#5150=ORIENTED_EDGE ( 'NONE', *, *, #20791, .T. ) ;
#5164=CARTESIAN_POINT ( 'NONE',  ( -0.2746410161513776482, -3.941790907013290823, -0.4709369376873030477 ) ) ;
#5165=EDGE_CURVE ( 'NONE', #4884, #25380, #2372, .T. ) ;
#5186=ORIENTED_EDGE ( 'NONE', *, *, #2706, .T. ) ;
#5195=ADVANCED_FACE ( 'NONE', ( #28390 ), #12919, .F. ) ;
#5199=EDGE_CURVE ( 'NONE', #14323, #36573, #32269, .T. ) ;
#5203=CYLINDRICAL_SURFACE ( 'NONE', #12537, 0.1000000000000000194 ) ;
#5209=DIRECTION ( 'NONE',  ( -0.5000000000000009992, -0.7066258520834616252, -0.5006794435238185459 ) ) ;
#5224=CARTESIAN_POINT ( 'NONE',  ( -0.2399999999999999079, -2.914247627487775105, -0.7567636692719127423 ) ) ;
#5242=ORIENTED_EDGE ( 'NONE', *, *, #25793, .F. ) ;
#5262=AXIS2_PLACEMENT_3D ( 'NONE', #26166, #10506, #20192 ) ;
#5269=DIRECTION ( 'NONE',  ( 0.000000000000000000, 1.707404996040147600E-15, -1.000000000000000000 ) ) ;
#5272=DIRECTION ( 'NONE',  ( 1.000000000000000000, 0.000000000000000000, 0.000000000000000000 ) ) ;
#5274=ORIENTED_EDGE ( 'NONE', *, *, #25537, .T. ) ;
#5291=DIRECTION ( 'NONE',  ( 1.000000000000000000, 0.000000000000000000, 0.000000000000000000 ) ) ;
#5300=DIRECTION ( 'NONE',  ( -1.000000000000000000, 0.000000000000000000, 0.000000000000000000 ) ) ;
#5311=DIRECTION ( 'NONE',  ( 0.000000000000000000, 0.000000000000000000, -1.000000000000000000 ) ) ;
#5334=CARTESIAN_POINT ( 'NONE',  ( -0.2746410161513782033, -2.183180860297908144, -0.4937760292030871079 ) ) ;
#5337=DIRECTION ( 'NONE',  ( -0.5000000000000012212, -0.3297230132044404183, -0.8008013077932520929 ) ) ;
#5376=ORIENTED_EDGE ( 'NONE', *, *, #27253, .F. ) ;
#5385=ORIENTED_EDGE ( 'NONE', *, *, #9431, .T. ) ;
#5391=CARTESIAN_POINT ( 'NONE',  ( -0.3000000000000000999, -2.183180860297908144, -0.4937760292030871079 ) ) ;
#5394=ORIENTED_EDGE ( 'NONE', *, *, #33707, .F. ) ;
#5418=EDGE_CURVE ( 'NONE', #354, #24980, #39173, .T. ) ;
#5426=DIRECTION ( 'NONE',  ( -1.000000000000000000, -0.000000000000000000, -0.000000000000000000 ) ) ;
#5431=CIRCLE ( 'NONE', #4154, 0.1000000000000000194 ) ;
#5444=EDGE_CURVE ( 'NONE', #26723, #478, #40270, .T. ) ;
#5460=DIRECTION ( 'NONE',  ( 1.000000000000000000, 0.000000000000000000, 0.000000000000000000 ) ) ;
#5464=LINE ( 'NONE', #24831, #27942 ) ;
#5471=EDGE_CURVE ( 'NONE', #21617, #17567, #20965, .T. ) ;
#5477=VECTOR ( 'NONE', #9786, 39.37007874015748143 ) ;
#5480=ORIENTED_EDGE ( 'NONE', *, *, #25219, .T. ) ;
#5487=DIRECTION ( 'NONE',  ( -1.000000000000000000, -0.000000000000000000, -0.000000000000000000 ) ) ;
#5513=CIRCLE ( 'NONE', #24593, 0.1000000000000000194 ) ;
#5529=CIRCLE ( 'NONE', #20679, 0.1000000000000000194 ) ;
#5551=ORIENTED_EDGE ( 'NONE', *, *, #33769, .F. ) ;
#5576=PLANE ( 'NONE',  #6732 ) ;
#5590=CARTESIAN_POINT ( 'NONE',  ( -0.3000000000000000999, -3.791721498889941255, -0.2726869407194119077 ) ) ;
#5598=AXIS2_PLACEMENT_3D ( 'NONE', #7003, #26337, #20176 ) ;
#5607=ORIENTED_EDGE ( 'NONE', *, *, #9676, .T. ) ;
#5622=EDGE_CURVE ( 'NONE', #31054, #40610, #33259, .T. ) ;
#5629=CONICAL_SURFACE ( 'NONE', #17481, 0.1600000000000005584, 1.047197551196598075 ) ;
#5638=LINE ( 'NONE', #20896, #7679 ) ;
#5663=EDGE_CURVE ( 'NONE', #20453, #40011, #1118, .T. ) ;
#5666=CARTESIAN_POINT ( 'NONE',  ( -0.3000000000000000999, -4.385325017590463226, -0.5985264029706663935 ) ) ;
#5674=EDGE_CURVE ( 'NONE', #33666, #6106, #18245, .T. ) ;
#5690=DIRECTION ( 'NONE',  ( 0.000000000000000000, 0.000000000000000000, -1.000000000000000000 ) ) ;
#5695=FACE_OUTER_BOUND ( 'NONE', #34716, .T. ) ;
#5703=CARTESIAN_POINT ( 'NONE',  ( -0.2399999999999999079, -3.478759481804464038, -0.3573324461326447543 ) ) ;
#5715=ADVANCED_FACE ( 'NONE', ( #20743 ), #18039, .F. ) ;
#5716=ORIENTED_EDGE ( 'NONE', *, *, #15694, .T. ) ;
#5721=EDGE_CURVE ( 'NONE', #28382, #14767, #29332, .T. ) ;
#5736=CARTESIAN_POINT ( 'NONE',  ( -0.2399999999999999079, -1.891808285041389093, -0.4498908273618595910 ) ) ;
#5740=EDGE_CURVE ( 'NONE', #20593, #33666, #14956, .T. ) ;
#5763=LINE ( 'NONE', #33527, #29238 ) ;
#5775=DIRECTION ( 'NONE',  ( 1.000000000000000000, 0.000000000000000000, 0.000000000000000000 ) ) ;
#5780=FACE_OUTER_BOUND ( 'NONE', #18681, .T. ) ;
#5784=DIRECTION ( 'NONE',  ( 1.000000000000000000, 0.000000000000000000, 0.000000000000000000 ) ) ;
#5799=ORIENTED_EDGE ( 'NONE', *, *, #15710, .F. ) ;
#5806=ORIENTED_EDGE ( 'NONE', *, *, #27739, .T. ) ;
#5813=ORIENTED_EDGE ( 'NONE', *, *, #24369, .F. ) ;
#5819=CARTESIAN_POINT ( 'NONE',  ( -0.3000000000000000999, -2.068584980338025847, -0.2731141320652225590 ) ) ;
#5828=DIRECTION ( 'NONE',  ( 1.000000000000000000, 0.000000000000000000, 0.000000000000000000 ) ) ;
#5830=CARTESIAN_POINT ( 'NONE',  ( -0.2746410161513776482, -3.849534981189179028, -0.1910928155360645808 ) ) ;
#5835=ORIENTED_EDGE ( 'NONE', *, *, #18262, .F. ) ;
#5838=ORIENTED_EDGE ( 'NONE', *, *, #6733, .F. ) ;
#5845=CARTESIAN_POINT ( 'NONE',  ( -0.2399999999999999079, -2.323257895298838971, -0.7902071827178637209 ) ) ;
#5848=ORIENTED_EDGE ( 'NONE', *, *, #20744, .T. ) ;
#5894=CARTESIAN_POINT ( 'NONE',  ( -0.3000000000000000999, -3.156018320128275878, -0.4841849112664152743 ) ) ;
#5903=EDGE_CURVE ( 'NONE', #1786, #27128, #5638, .T. ) ;
#5933=FACE_OUTER_BOUND ( 'NONE', #250, .T. ) ;
#5936=EDGE_CURVE ( 'NONE', #31618, #34948, #25440, .T. ) ;
#5943=DIRECTION ( 'NONE',  ( 0.000000000000000000, -1.047646519776162108E-15, -1.000000000000000000 ) ) ;
#5983=CARTESIAN_POINT ( 'NONE',  ( -0.2399999999999999079, -3.719155698466370286, -0.2948051799630662106 ) ) ;
#6001=CARTESIAN_POINT ( 'NONE',  ( -0.3000000000000000999, -3.941790907013290823, -0.4709369376873030477 ) ) ;
#6005=DIRECTION ( 'NONE',  ( 1.000000000000000000, 0.000000000000000000, 0.000000000000000000 ) ) ;
#6028=AXIS2_PLACEMENT_3D ( 'NONE', #14289, #35690, #30132 ) ;
#6039=ORIENTED_EDGE ( 'NONE', *, *, #12042, .F. ) ;
#6053=ORIENTED_EDGE ( 'NONE', *, *, #33366, .F. ) ;
#6057=DIRECTION ( 'NONE',  ( 1.000000000000000000, -0.000000000000000000, -0.000000000000000000 ) ) ;
#6065=EDGE_CURVE ( 'NONE', #6967, #30939, #12616, .T. ) ;
#6092=CARTESIAN_POINT ( 'NONE',  ( -0.2746410161513776482, -3.941790907013290823, -0.4709369376873030477 ) ) ;
#6104=DIRECTION ( 'NONE',  ( -1.000000000000000000, -0.000000000000000000, -0.000000000000000000 ) ) ;
#6106=VERTEX_POINT ( 'NONE', #24792 ) ;
#6115=ORIENTED_EDGE ( 'NONE', *, *, #21991, .F. ) ;
#6124=CIRCLE ( 'NONE', #4789, 0.06250000000000001388 ) ;
#6125=CARTESIAN_POINT ( 'NONE',  ( -0.3000000000000000999, -4.015775813216793999, -0.6509878610687880318 ) ) ;
#6154=ORIENTED_EDGE ( 'NONE', *, *, #16072, .T. ) ;
#6164=VECTOR ( 'NONE', #39498, 39.37007874015748143 ) ;
#6188=DIRECTION ( 'NONE',  ( 0.000000000000000000, 0.000000000000000000, -1.000000000000000000 ) ) ;
#6193=VECTOR ( 'NONE', #5209, 39.37007874015748854 ) ;
#6202=ORIENTED_EDGE ( 'NONE', *, *, #6065, .F. ) ;
#6205=CIRCLE ( 'NONE', #29214, 0.1946589359789743512 ) ;
#6208=ORIENTED_EDGE ( 'NONE', *, *, #17546, .T. ) ;
#6209=VECTOR ( 'NONE', #5460, 39.37007874015748143 ) ;
#6215=AXIS2_PLACEMENT_3D ( 'NONE', #35485, #7289, #32008 ) ;
#6216=VECTOR ( 'NONE', #1891, 39.37007874015748854 ) ;
#6222=ORIENTED_EDGE ( 'NONE', *, *, #26367, .F. ) ;
#6230=EDGE_CURVE ( 'NONE', #40011, #39872, #11625, .T. ) ;
#6246=ADVANCED_FACE ( 'NONE', ( #10548 ), #19811, .F. ) ;
#6247=EDGE_CURVE ( 'NONE', #8621, #20383, #10152, .T. ) ;
#6249=CONICAL_SURFACE ( 'NONE', #9546, 0.1599999999999999201, 1.047197551196601406 ) ;
#6258=ORIENTED_EDGE ( 'NONE', *, *, #16789, .T. ) ;
#6260=LINE ( 'NONE', #15535, #11978 ) ;
#6261=CARTESIAN_POINT ( 'NONE',  ( -0.3000000000000000999, -3.194091454214595949, -0.5766534813907828738 ) ) ;
#6266=VERTEX_POINT ( 'NONE', #7238 ) ;
#6309=CARTESIAN_POINT ( 'NONE',  ( -0.2399999999999999079, -3.253611865733782693, -0.3464478357516359575 ) ) ;
#6310=DIRECTION ( 'NONE',  ( 0.000000000000000000, 0.000000000000000000, 1.000000000000000000 ) ) ;
#6332=DIRECTION ( 'NONE',  ( 0.000000000000000000, 0.000000000000000000, -1.000000000000000000 ) ) ;
#6337=CARTESIAN_POINT ( 'NONE',  ( -0.2399999999999999079, -3.941790907013290823, -0.4709369376873030477 ) ) ;
#6348=VERTEX_POINT ( 'NONE', #13442 ) ;
#6354=EDGE_CURVE ( 'NONE', #31920, #6106, #38530, .T. ) ;
#6357=AXIS2_PLACEMENT_3D ( 'NONE', #25111, #34361, #8862 ) ;
#6358=ORIENTED_EDGE ( 'NONE', *, *, #11992, .T. ) ;
#6366=ORIENTED_EDGE ( 'NONE', *, *, #5165, .T. ) ;
#6382=LINE ( 'NONE', #35192, #29275 ) ;
#6385=DIRECTION ( 'NONE',  ( -1.000000000000000000, -0.000000000000000000, -0.000000000000000000 ) ) ;
#6399=EDGE_CURVE ( 'NONE', #37899, #839, #5026, .T. ) ;
#6410=EDGE_LOOP ( 'NONE', ( #17000, #9465, #9950, #3582 ) ) ;
#6412=CARTESIAN_POINT ( 'NONE',  ( -0.3000000000000000999, -2.289343986263487896, -0.6686455968847019316 ) ) ;
#6430=DIRECTION ( 'NONE',  ( 0.000000000000000000, 0.000000000000000000, -1.000000000000000000 ) ) ;
#6440=ORIENTED_EDGE ( 'NONE', *, *, #10499, .F. ) ;
#6441=LINE ( 'NONE', #938, #14798 ) ;
#6473=EDGE_CURVE ( 'NONE', #29444, #38406, #37065, .T. ) ;
#6497=DIRECTION ( 'NONE',  ( 0.000000000000000000, 0.000000000000000000, -1.000000000000000000 ) ) ;
#6517=ORIENTED_EDGE ( 'NONE', *, *, #19111, .F. ) ;
#6524=DIRECTION ( 'NONE',  ( 0.000000000000000000, 0.000000000000000000, -1.000000000000000000 ) ) ;
#6527=EDGE_LOOP ( 'NONE', ( #27167, #1812, #25820, #2784 ) ) ;
#6531=LINE ( 'NONE', #12718, #40272 ) ;
#6538=DIRECTION ( 'NONE',  ( 0.000000000000000000, 0.000000000000000000, -1.000000000000000000 ) ) ;
#6548=DIRECTION ( 'NONE',  ( -1.000000000000000000, -0.000000000000000000, -0.000000000000000000 ) ) ;
#6555=VERTEX_POINT ( 'NONE', #9493 ) ;
#6564=CARTESIAN_POINT ( 'NONE',  ( -0.2399999999999999079, -4.098813193844367042, -0.6491724279539748954 ) ) ;
#6567=EDGE_LOOP ( 'NONE', ( #32803, #39043, #32309, #2441 ) ) ;
#6577=CARTESIAN_POINT ( 'NONE',  ( -0.2399999999999999079, -3.579933075828129141, -0.2145427270617869253 ) ) ;
#6586=EDGE_CURVE ( 'NONE', #27450, #24506, #7032, .T. ) ;
#6600=ORIENTED_EDGE ( 'NONE', *, *, #16291, .T. ) ;
#6613=ORIENTED_EDGE ( 'NONE', *, *, #30356, .T. ) ;
#6614=AXIS2_PLACEMENT_3D ( 'NONE', #37148, #15551, #21326 ) ;
#6621=LINE ( 'NONE', #31353, #8116 ) ;
#6625=EDGE_CURVE ( 'NONE', #34849, #17560, #29018, .T. ) ;
#6637=AXIS2_PLACEMENT_3D ( 'NONE', #35667, #19637, #4576 ) ;
#6653=CARTESIAN_POINT ( 'NONE',  ( -0.2399999999999999079, -4.292451985131092940, -0.8428112192407016812 ) ) ;
#6654=CARTESIAN_POINT ( 'NONE',  ( -0.2746410161513779258, -2.595429044015121534, -0.5484989581857646623 ) ) ;
#6658=ORIENTED_EDGE ( 'NONE', *, *, #15821, .F. ) ;
#6679=VECTOR ( 'NONE', #19169, 39.37007874015748854 ) ;
#6699=ADVANCED_FACE ( 'NONE', ( #13177 ), #38273, .T. ) ;
#6726=ORIENTED_EDGE ( 'NONE', *, *, #14539, .T. ) ;
#6732=AXIS2_PLACEMENT_3D ( 'NONE', #40127, #8654, #20626 ) ;
#6733=EDGE_CURVE ( 'NONE', #2349, #38034, #37257, .T. ) ;
#6734=CARTESIAN_POINT ( 'NONE',  ( -0.2746410161513776482, -3.941790907013290823, -0.2762780017083287243 ) ) ;
#6750=LINE ( 'NONE', #21803, #23887 ) ;
#6755=DIRECTION ( 'NONE',  ( 0.000000000000000000, 0.000000000000000000, 1.000000000000000000 ) ) ;
#6766=VERTEX_POINT ( 'NONE', #9893 ) ;
#6780=DIRECTION ( 'NONE',  ( -0.4999999999999972800, -0.8563665354314757838, -0.1289820025937487569 ) ) ;
#6801=AXIS2_PLACEMENT_3D ( 'NONE', #20224, #10963, #23523 ) ;
#6812=ORIENTED_EDGE ( 'NONE', *, *, #3599, .T. ) ;
#6849=DIRECTION ( 'NONE',  ( -1.000000000000000000, 0.000000000000000000, 0.000000000000000000 ) ) ;
#6874=DIRECTION ( 'NONE',  ( 0.4999999999999978351, 0.7308273574226412661, 0.4646411234949410218 ) ) ;
#6879=CARTESIAN_POINT ( 'NONE',  ( -0.2399999999999999079, -2.183180860297908144, -0.5562760292030870524 ) ) ;
#6883=AXIS2_PLACEMENT_3D ( 'NONE', #38173, #35303, #9997 ) ;
#6903=CIRCLE ( 'NONE', #22713, 0.1000000000000000194 ) ;
#6907=ORIENTED_EDGE ( 'NONE', *, *, #29276, .F. ) ;
#6908=EDGE_CURVE ( 'NONE', #10935, #19587, #1472, .T. ) ;
#6922=AXIS2_PLACEMENT_3D ( 'NONE', #2467, #15001, #40079 ) ;
#6967=VERTEX_POINT ( 'NONE', #5127 ) ;
#6972=DIRECTION ( 'NONE',  ( -1.000000000000000000, -0.000000000000000000, -0.000000000000000000 ) ) ;
#7003=CARTESIAN_POINT ( 'NONE',  ( -0.2399999999999999079, -3.253611865733782693, -0.3464478357516359575 ) ) ;
#7006=CARTESIAN_POINT ( 'NONE',  ( -0.2399999999999999079, -2.511040369707300268, -0.4948468226404901804 ) ) ;
#7026=VERTEX_POINT ( 'NONE', #11919 ) ;
#7032=CIRCLE ( 'NONE', #3757, 0.1600000000000006140 ) ;
#7040=CARTESIAN_POINT ( 'NONE',  ( -0.2746410161513779258, -2.068584980338025847, -0.2731141320652225035 ) ) ;
#7057=DIRECTION ( 'NONE',  ( 0.000000000000000000, -0.8159412518334721032, -0.5781348229923762849 ) ) ;
#7062=ORIENTED_EDGE ( 'NONE', *, *, #20744, .F. ) ;
#7075=VERTEX_POINT ( 'NONE', #40515 ) ;
#7085=CARTESIAN_POINT ( 'NONE',  ( -0.2399999999999999079, -2.183180860297908144, -0.4937760292030871079 ) ) ;
#7088=CARTESIAN_POINT ( 'NONE',  ( -0.2746410161513779258, -2.457388234162025675, -0.5792354969483111127 ) ) ;
#7099=ORIENTED_EDGE ( 'NONE', *, *, #34401, .T. ) ;
#7108=CARTESIAN_POINT ( 'NONE',  ( -0.2746410161513770931, -2.878813263491020180, -0.3823467908819087602 ) ) ;
#7126=CARTESIAN_POINT ( 'NONE',  ( -0.3000000000000000999, -3.941790907013290823, -0.4084369376873030477 ) ) ;
#7129=CARTESIAN_POINT ( 'NONE',  ( -0.2399999999999999079, -3.525450504378606187, -0.1357627943591874498 ) ) ;
#7131=EDGE_CURVE ( 'NONE', #26308, #19197, #37840, .T. ) ;
#7159=ORIENTED_EDGE ( 'NONE', *, *, #15821, .T. ) ;
#7171=ORIENTED_EDGE ( 'NONE', *, *, #13249, .T. ) ;
#7192=DIRECTION ( 'NONE',  ( -0.4999999999999991118, 0.5006794435238204333, -0.7066258520834617363 ) ) ;
#7205=EDGE_CURVE ( 'NONE', #27945, #24904, #13342, .T. ) ;
#7208=CARTESIAN_POINT ( 'NONE',  ( -0.2399999999999999079, -2.183180860297908144, -0.4937760292030871079 ) ) ;
#7217=CARTESIAN_POINT ( 'NONE',  ( -0.2399999999999999079, -2.341127044584462968, -0.9908042926600856282 ) ) ;
#7238=CARTESIAN_POINT ( 'NONE',  ( -0.2746410161513779258, -3.747168848490688209, -0.4747258284076885104 ) ) ;
#7239=DIRECTION ( 'NONE',  ( -0.8660254037844403729, -0.4219433715391017192, -0.2682606777263723541 ) ) ;
#7244=CARTESIAN_POINT ( 'NONE',  ( -0.2399999999999999079, -2.322955634169589612, -0.9336221289765171960 ) ) ;
#7246=EDGE_CURVE ( 'NONE', #40610, #32592, #30978, .T. ) ;
#7254=CARTESIAN_POINT ( 'NONE',  ( -0.2399999999999999079, -3.268524983732795874, -0.6433364877554555994 ) ) ;
#7266=ORIENTED_EDGE ( 'NONE', *, *, #37914, .F. ) ;
#7271=DIRECTION ( 'NONE',  ( 1.000000000000000000, -0.000000000000000000, -0.000000000000000000 ) ) ;
#7278=AXIS2_PLACEMENT_3D ( 'NONE', #13297, #37990, #25868 ) ;
#7281=VECTOR ( 'NONE', #8570, 39.37007874015748854 ) ;
#7289=DIRECTION ( 'NONE',  ( -1.000000000000000000, -0.000000000000000000, -0.000000000000000000 ) ) ;
#7314=FACE_OUTER_BOUND ( 'NONE', #1704, .T. ) ;
#7323=ORIENTED_EDGE ( 'NONE', *, *, #29833, .F. ) ;
#7338=ADVANCED_BREP_SHAPE_REPRESENTATION ( '', ( #4819, #27819 ), #33713 ) ;
#7343=VECTOR ( 'NONE', #12850, 39.37007874015748143 ) ;
#7347=ORIENTED_EDGE ( 'NONE', *, *, #16129, .F. ) ;
#7358=DIRECTION ( 'NONE',  ( 0.000000000000000000, 0.000000000000000000, -1.000000000000000000 ) ) ;
#7359=ORIENTED_EDGE ( 'NONE', *, *, #26983, .T. ) ;
#7382=CARTESIAN_POINT ( 'NONE',  ( -0.2399999999999999079, -2.853330612949663170, -0.6088139570729240724 ) ) ;
#7386=CARTESIAN_POINT ( 'NONE',  ( -0.2399999999999999079, -1.835749455202394298, -0.2938319975228648739 ) ) ;
#7395=VECTOR ( 'NONE', #12118, 39.37007874015748854 ) ;
#7399=ORIENTED_EDGE ( 'NONE', *, *, #3993, .T. ) ;
#7400=ORIENTED_EDGE ( 'NONE', *, *, #23306, .T. ) ;
#7407=EDGE_LOOP ( 'NONE', ( #40462, #40090, #24567, #1969 ) ) ;
#7421=VERTEX_POINT ( 'NONE', #15714 ) ;
#7437=DIRECTION ( 'NONE',  ( -0.8660254037844407060, 0.2890674114961861441, -0.4079706259167332760 ) ) ;
#7448=VECTOR ( 'NONE', #27974, 39.37007874015748143 ) ;
#7451=AXIS2_PLACEMENT_3D ( 'NONE', #37329, #28842, #21921 ) ;
#7460=DIRECTION ( 'NONE',  ( 0.000000000000000000, 0.8438867430782092116, 0.5365213554527465956 ) ) ;
#7463=ORIENTED_EDGE ( 'NONE', *, *, #17439, .F. ) ;
#7490=EDGE_CURVE ( 'NONE', #19496, #14090, #28680, .T. ) ;
#7500=ORIENTED_EDGE ( 'NONE', *, *, #32417, .T. ) ;
#7505=VECTOR ( 'NONE', #25493, 39.37007874015748143 ) ;
#7510=CARTESIAN_POINT ( 'NONE',  ( -0.2399999999999999079, -2.183180860297908144, -0.4937760292030871079 ) ) ;
#7521=ADVANCED_FACE ( 'NONE', ( #731 ), #22516, .T. ) ;
#7528=EDGE_LOOP ( 'NONE', ( #16645, #29863, #30407, #1852 ) ) ;
#7530=ORIENTED_EDGE ( 'NONE', *, *, #20237, .T. ) ;
#7548=CARTESIAN_POINT ( 'NONE',  ( -0.2399999999999999079, -3.807157481699992907, -0.4735579732456337565 ) ) ;
#7551=CARTESIAN_POINT ( 'NONE',  ( -0.3000000000000000999, -2.768941938641841904, -0.5551618215276492574 ) ) ;
#7575=CARTESIAN_POINT ( 'NONE',  ( -0.2746410161513776482, -3.723902497147952406, 0.1004495357399106253 ) ) ;
#7581=VERTEX_POINT ( 'NONE', #1139 ) ;
#7591=AXIS2_PLACEMENT_3D ( 'NONE', #6337, #33160, #18909 ) ;
#7603=CARTESIAN_POINT ( 'NONE',  ( -0.2399999999999999079, -3.941790907013290823, -0.4709369376873030477 ) ) ;
#7608=EDGE_CURVE ( 'NONE', #31622, #4130, #692, .T. ) ;
#7612=CARTESIAN_POINT ( 'NONE',  ( -0.2399999999999999079, -3.941790907013290823, -0.5334369376873030477 ) ) ;
#7614=EDGE_CURVE ( 'NONE', #11375, #19638, #35810, .T. ) ;
#7632=CARTESIAN_POINT ( 'NONE',  ( -0.2746410161513782033, -2.289343986263487896, -0.6686455968847019316 ) ) ;
#7636=DIRECTION ( 'NONE',  ( -0.4999999999999995559, 0.6123724356957945814, -0.6123724356957945814 ) ) ;
#7669=ADVANCED_FACE ( 'NONE', ( #4123 ), #13604, .T. ) ;
#7672=EDGE_CURVE ( 'NONE', #16220, #15882, #40092, .T. ) ;
#7679=VECTOR ( 'NONE', #2164, 39.37007874015748143 ) ;
#7686=DIRECTION ( 'NONE',  ( 1.000000000000000000, 0.000000000000000000, 0.000000000000000000 ) ) ;
#7690=EDGE_LOOP ( 'NONE', ( #26634, #15973, #16246, #25355 ) ) ;
#7707=CARTESIAN_POINT ( 'NONE',  ( -0.2746410161513770931, -3.194091454214595949, -0.5766534813907827628 ) ) ;
#7714=ADVANCED_FACE ( 'NONE', ( #8018 ), #14460, .F. ) ;
#7736=CARTESIAN_POINT ( 'NONE',  ( -0.2399999999999999079, -3.950462929358175668, -0.4586978189098018799 ) ) ;
#7758=ADVANCED_FACE ( 'NONE', ( #2282 ), #14821, .T. ) ;
#7768=DIRECTION ( 'NONE',  ( 1.000000000000000000, -0.000000000000000000, -0.000000000000000000 ) ) ;
#7782=CARTESIAN_POINT ( 'NONE',  ( -0.2399999999999999079, -3.840189043187996809, -0.1239867222638698224 ) ) ;
#7820=ORIENTED_EDGE ( 'NONE', *, *, #24403, .T. ) ;
#7822=EDGE_LOOP ( 'NONE', ( #30313, #24698, #20434, #10232, #6600, #30565, #11796, #37746, #16398, #39406, #33696 ) ) ;
#7863=EDGE_LOOP ( 'NONE', ( #17806, #28932, #24293, #3280 ) ) ;
#7876=VECTOR ( 'NONE', #25696, 39.37007874015748854 ) ;
#7883=ADVANCED_FACE ( 'NONE', ( #34340 ), #24983, .F. ) ;
#7893=CARTESIAN_POINT ( 'NONE',  ( -0.3000000000000000999, -3.941790907013290823, -0.4709369376873030477 ) ) ;
#7900=ORIENTED_EDGE ( 'NONE', *, *, #3141, .T. ) ;
#7906=CARTESIAN_POINT ( 'NONE',  ( -0.2399999999999999079, -3.941790907013290823, -0.4709369376873030477 ) ) ;
#7924=DIRECTION ( 'NONE',  ( 0.000000000000000000, -3.414809992080318866E-15, -1.000000000000000000 ) ) ;
#7930=EDGE_CURVE ( 'NONE', #35757, #3317, #2670, .T. ) ;
#7933=ADVANCED_FACE ( 'NONE', ( #37423 ), #26987, .T. ) ;
#7966=DIRECTION ( 'NONE',  ( 0.000000000000000000, 0.000000000000000000, 1.000000000000000000 ) ) ;
#7983=EDGE_CURVE ( 'NONE', #35098, #23694, #9888, .T. ) ;
#7984=DIRECTION ( 'NONE',  ( 0.8660254037844381525, 0.3535533905932748966, -0.3535533905932738974 ) ) ;
#7997=DIRECTION ( 'NONE',  ( 1.000000000000000000, 0.000000000000000000, 0.000000000000000000 ) ) ;
#8015=VERTEX_POINT ( 'NONE', #23027 ) ;
#8018=FACE_OUTER_BOUND ( 'NONE', #8355, .T. ) ;
#8019=AXIS2_PLACEMENT_3D ( 'NONE', #28109, #37542, #34064 ) ;
#8022=EDGE_LOOP ( 'NONE', ( #31111, #36812 ) ) ;
#8031=FACE_OUTER_BOUND ( 'NONE', #15072, .T. ) ;
#8059=AXIS2_PLACEMENT_3D ( 'NONE', #30792, #2613, #34684 ) ;
#8066=ORIENTED_EDGE ( 'NONE', *, *, #37674, .T. ) ;
#8087=AXIS2_PLACEMENT_3D ( 'NONE', #11861, #2220, #15363 ) ;
#8094=ORIENTED_EDGE ( 'NONE', *, *, #16965, .T. ) ;
#8111=DIRECTION ( 'NONE',  ( -1.000000000000000000, -0.000000000000000000, -0.000000000000000000 ) ) ;
#8114=EDGE_CURVE ( 'NONE', #839, #26723, #16043, .T. ) ;
#8116=VECTOR ( 'NONE', #9928, 39.37007874015748143 ) ;
#8137=DIRECTION ( 'NONE',  ( 1.000000000000000000, 0.000000000000000000, 0.000000000000000000 ) ) ;
#8142=CARTESIAN_POINT ( 'NONE',  ( -0.2746410161513782033, -1.906460133321048911, -0.3231213194042101278 ) ) ;
#8172=EDGE_CURVE ( 'NONE', #24406, #27585, #647, .T. ) ;
#8189=CARTESIAN_POINT ( 'NONE',  ( -0.2746410161513779258, -3.667123564397057667, -0.3682398926280779361 ) ) ;
#8208=AXIS2_PLACEMENT_3D ( 'NONE', #36101, #26449, #10820 ) ;
#8243=CYLINDRICAL_SURFACE ( 'NONE', #30533, 0.1000000000000000194 ) ;
#8248=ORIENTED_EDGE ( 'NONE', *, *, #21376, .T. ) ;
#8259=CYLINDRICAL_SURFACE ( 'NONE', #7591, 0.1946589359789743512 ) ;
#8293=ORIENTED_EDGE ( 'NONE', *, *, #1666, .F. ) ;
#8299=CARTESIAN_POINT ( 'NONE',  ( -0.2746410161513782033, -1.990692974992658737, -0.4647843861454829528 ) ) ;
#8315=DIRECTION ( 'NONE',  ( 1.000000000000000000, 0.000000000000000000, 0.000000000000000000 ) ) ;
#8323=VECTOR ( 'NONE', #2713, 39.37007874015748854 ) ;
#8326=LINE ( 'NONE', #17178, #19907 ) ;
#8344=DIRECTION ( 'NONE',  ( 0.000000000000000000, 0.000000000000000000, -1.000000000000000000 ) ) ;
#8349=LINE ( 'NONE', #8538, #4908 ) ;
#8355=EDGE_LOOP ( 'NONE', ( #34852, #38658, #27353, #1851, #19887 ) ) ;
#8400=ADVANCED_FACE ( 'NONE', ( #17245 ), #1638, .F. ) ;
#8409=CARTESIAN_POINT ( 'NONE',  ( -0.3000000000000000999, -3.217981293616048344, -0.2530108926800492264 ) ) ;
#8428=EDGE_LOOP ( 'NONE', ( #39487, #23795, #20863, #5799 ) ) ;
#8452=ADVANCED_FACE ( 'NONE', ( #8572 ), #15824, .T. ) ;
#8457=FACE_OUTER_BOUND ( 'NONE', #12824, .T. ) ;
#8487=ORIENTED_EDGE ( 'NONE', *, *, #14172, .T. ) ;
#8506=FACE_OUTER_BOUND ( 'NONE', #14597, .T. ) ;
#8521=ORIENTED_EDGE ( 'NONE', *, *, #23599, .T. ) ;
#8538=CARTESIAN_POINT ( 'NONE',  ( -0.2746410161513776482, -3.838583118162426810, -0.3058907208964237734 ) ) ;
#8544=EDGE_CURVE ( 'NONE', #8729, #4884, #33906, .T. ) ;
#8556=AXIS2_PLACEMENT_3D ( 'NONE', #3273, #21811, #5943 ) ;
#8557=DIRECTION ( 'NONE',  ( 1.000000000000000000, -0.000000000000000000, -0.000000000000000000 ) ) ;
#8560=LINE ( 'NONE', #24638, #27176 ) ;
#8567=CARTESIAN_POINT ( 'NONE',  ( -0.3000000000000000999, -3.941790907013290823, -0.4709369376873030477 ) ) ;
#8570=DIRECTION ( 'NONE',  ( -0.4999999999999993894, 0.3085698060533125786, 0.8091876635195458523 ) ) ;
#8572=FACE_OUTER_BOUND ( 'NONE', #24905, .T. ) ;
#8576=DIRECTION ( 'NONE',  ( 0.000000000000000000, 0.000000000000000000, -1.000000000000000000 ) ) ;
#8582=LINE ( 'NONE', #31561, #29101 ) ;
#8588=CARTESIAN_POINT ( 'NONE',  ( -0.2746410161513779258, -4.250025578259899461, -0.8852376261118947154 ) ) ;
#8590=AXIS2_PLACEMENT_3D ( 'NONE', #38003, #13308, #16600 ) ;
#8609=LINE ( 'NONE', #30651, #35644 ) ;
#8614=DIRECTION ( 'NONE',  ( 1.000000000000000000, 0.000000000000000000, 0.000000000000000000 ) ) ;
#8621=VERTEX_POINT ( 'NONE', #9186 ) ;
#8624=DIRECTION ( 'NONE',  ( -1.000000000000000000, 0.000000000000000000, 0.000000000000000000 ) ) ;
#8627=ADVANCED_FACE ( 'NONE', ( #19877 ), #23733, .F. ) ;
#8644=VECTOR ( 'NONE', #37662, 39.37007874015748143 ) ;
#8654=DIRECTION ( 'NONE',  ( 1.000000000000000000, 0.000000000000000000, 0.000000000000000000 ) ) ;
#8682=ORIENTED_EDGE ( 'NONE', *, *, #17428, .T. ) ;
#8684=DIRECTION ( 'NONE',  ( 1.000000000000000000, -0.000000000000000000, -0.000000000000000000 ) ) ;
#8725=EDGE_LOOP ( 'NONE', ( #2727, #39443, #35601, #34546 ) ) ;
#8729=VERTEX_POINT ( 'NONE', #9607 ) ;
#8731=AXIS2_PLACEMENT_3D ( 'NONE', #27373, #15414, #27972 ) ;
#8740=CARTESIAN_POINT ( 'NONE',  ( -0.2399999999999999079, -3.941790907013290823, -0.5334369376873030477 ) ) ;
#8751=EDGE_CURVE ( 'NONE', #1392, #27226, #15203, .T. ) ;
#8754=DIRECTION ( 'NONE',  ( 0.5000000000000019984, 0.6123724356957942483, -0.6123724356957930270 ) ) ;
#8769=AXIS2_PLACEMENT_3D ( 'NONE', #17039, #7768, #29578 ) ;
#8778=CIRCLE ( 'NONE', #7451, 0.1000000000000000194 ) ;
#8780=DIRECTION ( 'NONE',  ( 1.000000000000000000, 0.000000000000000000, 0.000000000000000000 ) ) ;
#8789=CARTESIAN_POINT ( 'NONE',  ( -0.2746410161513782033, -2.183180860297908144, -0.4937760292030871079 ) ) ;
#8794=LINE ( 'NONE', #24442, #21981 ) ;
#8812=AXIS2_PLACEMENT_3D ( 'NONE', #3606, #15555, #369 ) ;
#8816=DIRECTION ( 'NONE',  ( -0.8660254037844401509, -0.2682606777263719100, 0.4219433715391024964 ) ) ;
#8818=DIRECTION ( 'NONE',  ( 0.4999999999999943379, -0.3297230132044419726, -0.8008013077932559787 ) ) ;
#8843=DIRECTION ( 'NONE',  ( 1.000000000000000000, -0.000000000000000000, -0.000000000000000000 ) ) ;
#8847=ORIENTED_EDGE ( 'NONE', *, *, #24325, .T. ) ;
#8859=AXIS2_PLACEMENT_3D ( 'NONE', #14469, #21495, #2354 ) ;
#8862=DIRECTION ( 'NONE',  ( 0.000000000000000000, 0.000000000000000000, -1.000000000000000000 ) ) ;
#8867=DIRECTION ( 'NONE',  ( 0.000000000000000000, 0.000000000000000000, -1.000000000000000000 ) ) ;
#8877=CARTESIAN_POINT ( 'NONE',  ( -0.2399999999999999079, -4.442986640879458271, -0.6151136631325511139 ) ) ;
#8878=EDGE_CURVE ( 'NONE', #40516, #19999, #39399, .T. ) ;
#8883=AXIS2_PLACEMENT_3D ( 'NONE', #3666, #32441, #32045 ) ;
#8885=CARTESIAN_POINT ( 'NONE',  ( -0.2746410161513779258, -1.874946189051298617, -0.07947534077849525980 ) ) ;
#8888=ORIENTED_EDGE ( 'NONE', *, *, #4230, .F. ) ;
#8896=CIRCLE ( 'NONE', #19427, 0.1346589359789737705 ) ;
#8904=ORIENTED_EDGE ( 'NONE', *, *, #35806, .T. ) ;
#8915=AXIS2_PLACEMENT_3D ( 'NONE', #28860, #18809, #6430 ) ;
#8917=EDGE_CURVE ( 'NONE', #14679, #33134, #18494, .T. ) ;
#8920=CARTESIAN_POINT ( 'NONE',  ( 0.000000000000000000, 0.000000000000000000, 0.000000000000000000 ) ) ;
#8923=CARTESIAN_POINT ( 'NONE',  ( -0.2399999999999999079, -2.458279774191353351, -0.8760505995903041798 ) ) ;
#8939=AXIS2_PLACEMENT_3D ( 'NONE', #13575, #10075, #259 ) ;
#8950=DIRECTION ( 'NONE',  ( 1.000000000000000000, -0.000000000000000000, -0.000000000000000000 ) ) ;
#8970=ADVANCED_FACE ( 'NONE', ( #36313 ), #2730, .T. ) ;
#8988=AXIS2_PLACEMENT_3D ( 'NONE', #38009, #16399, #31633 ) ;
#8991=VERTEX_POINT ( 'NONE', #40424 ) ;
#8992=PLANE ( 'NONE',  #9510 ) ;
#8998=EDGE_LOOP ( 'NONE', ( #34812, #13603, #34661, #3978 ) ) ;
#9000=EDGE_CURVE ( 'NONE', #33695, #20593, #15856, .T. ) ;
#9001=VERTEX_POINT ( 'NONE', #14504 ) ;
#9015=ORIENTED_EDGE ( 'NONE', *, *, #14710, .T. ) ;
#9029=EDGE_CURVE ( 'NONE', #22735, #20761, #16527, .T. ) ;
#9036=DIRECTION ( 'NONE',  ( -1.000000000000000000, -0.000000000000000000, -0.000000000000000000 ) ) ;
#9052=CARTESIAN_POINT ( 'NONE',  ( -0.2399999999999999079, -2.375187403135927688, -0.6336237179921873075 ) ) ;
#9053=CARTESIAN_POINT ( 'NONE',  ( -0.2399999999999999079, -2.810395079000055585, -0.3781292493067240912 ) ) ;
#9066=VERTEX_POINT ( 'NONE', #8740 ) ;
#9069=CARTESIAN_POINT ( 'NONE',  ( -0.2399999999999999079, -2.342996121808762044, -0.6842569225768811991 ) ) ;
#9077=CARTESIAN_POINT ( 'NONE',  ( -0.2746410161513776482, -4.121841830394775030, -0.5449218438908057793 ) ) ;
#9078=CARTESIAN_POINT ( 'NONE',  ( -0.2399999999999999079, -3.941790907013290823, -0.4709369376873030477 ) ) ;
#9087=ORIENTED_EDGE ( 'NONE', *, *, #32560, .T. ) ;
#9095=VERTEX_POINT ( 'NONE', #33434 ) ;
#9097=DIRECTION ( 'NONE',  ( -1.000000000000000000, -0.000000000000000000, -0.000000000000000000 ) ) ;
#9101=ORIENTED_EDGE ( 'NONE', *, *, #17925, .F. ) ;
#9149=CARTESIAN_POINT ( 'NONE',  ( -0.2399999999999999079, -2.457388234162025675, -0.5792354969483111127 ) ) ;
#9155=CARTESIAN_POINT ( 'NONE',  ( -0.2746410161513770931, -2.861028283584748699, -0.4103205306338891245 ) ) ;
#9160=ADVANCED_FACE ( 'NONE', ( #13056 ), #9943, .F. ) ;
#9183=ADVANCED_FACE ( 'NONE', ( #16348 ), #13251, .F. ) ;
#9186=CARTESIAN_POINT ( 'NONE',  ( -0.2746410161513776482, -4.289222312108804225, -0.6708809693675255037 ) ) ;
#9204=VECTOR ( 'NONE', #18929, 39.37007874015748854 ) ;
#9226=FACE_OUTER_BOUND ( 'NONE', #7863, .T. ) ;
#9227=DIRECTION ( 'NONE',  ( -0.4999999999999985567, -0.6123724356957951365, 0.6123724356957951365 ) ) ;
#9228=AXIS2_PLACEMENT_3D ( 'NONE', #26638, #7686, #39167 ) ;
#9231=ORIENTED_EDGE ( 'NONE', *, *, #9029, .F. ) ;
#9243=VERTEX_POINT ( 'NONE', #36484 ) ;
#9248=DIRECTION ( 'NONE',  ( -1.000000000000000000, -0.000000000000000000, -0.000000000000000000 ) ) ;
#9250=CARTESIAN_POINT ( 'NONE',  ( -0.2746410161513770931, -2.909786385774835171, -0.3705357231075772084 ) ) ;
#9260=AXIS2_PLACEMENT_3D ( 'NONE', #7782, #39059, #4894 ) ;
#9271=AXIS2_PLACEMENT_3D ( 'NONE', #23425, #32648, #33448 ) ;
#9277=CARTESIAN_POINT ( 'NONE',  ( -0.3000000000000000999, -2.375007723916885194, -0.5268601001523036675 ) ) ;
#9281=DIRECTION ( 'NONE',  ( 1.000000000000000000, -0.000000000000000000, -0.000000000000000000 ) ) ;
#9286=ADVANCED_FACE ( 'NONE', ( #2342 ), #14881, .F. ) ;
#9295=CIRCLE ( 'NONE', #3399, 0.4615209409081865166 ) ;
#9301=ORIENTED_EDGE ( 'NONE', *, *, #8751, .F. ) ;
#9308=ORIENTED_EDGE ( 'NONE', *, *, #23626, .T. ) ;
#9313=VECTOR ( 'NONE', #18689, 39.37007874015748143 ) ;
#9331=VERTEX_POINT ( 'NONE', #39769 ) ;
#9348=CIRCLE ( 'NONE', #10039, 0.1000000000000000194 ) ;
#9357=VECTOR ( 'NONE', #10512, 39.37007874015748854 ) ;
#9378=FACE_OUTER_BOUND ( 'NONE', #18771, .T. ) ;
#9397=DIRECTION ( 'NONE',  ( -1.000000000000000000, 0.000000000000000000, 0.000000000000000000 ) ) ;
#9398=DIRECTION ( 'NONE',  ( 0.000000000000000000, 0.000000000000000000, 1.000000000000000000 ) ) ;
#9411=VERTEX_POINT ( 'NONE', #37478 ) ;
#9420=CARTESIAN_POINT ( 'NONE',  ( -0.2746410161513782033, -2.294529520598973082, -0.6534431116140350104 ) ) ;
#9422=AXIS2_PLACEMENT_3D ( 'NONE', #34482, #25849, #3410 ) ;
#9431=EDGE_CURVE ( 'NONE', #6766, #9411, #32313, .T. ) ;
#9433=CARTESIAN_POINT ( 'NONE',  ( -0.2399999999999999079, -2.183180860297908144, -0.4937760292030871079 ) ) ;
#9438=DIRECTION ( 'NONE',  ( 1.000000000000000000, -0.000000000000000000, -0.000000000000000000 ) ) ;
#9440=CARTESIAN_POINT ( 'NONE',  ( -0.2746410161513770931, -2.768941938641841904, -0.5551618215276492574 ) ) ;
#9443=ORIENTED_EDGE ( 'NONE', *, *, #26822, .F. ) ;
#9450=DIRECTION ( 'NONE',  ( 0.000000000000000000, 0.000000000000000000, -1.000000000000000000 ) ) ;
#9453=AXIS2_PLACEMENT_3D ( 'NONE', #7906, #39205, #35486 ) ;
#9465=ORIENTED_EDGE ( 'NONE', *, *, #33873, .F. ) ;
#9468=CARTESIAN_POINT ( 'NONE',  ( -0.2399999999999999079, -3.941790907013290823, -0.4709369376873030477 ) ) ;
#9469=CARTESIAN_POINT ( 'NONE',  ( -0.2746410161513779258, -4.394818335734379744, -0.8816972205720928768 ) ) ;
#9473=VECTOR ( 'NONE', #38780, 39.37007874015748854 ) ;
#9475=AXIS2_PLACEMENT_3D ( 'NONE', #13239, #22729, #7057 ) ;
#9486=EDGE_CURVE ( 'NONE', #22735, #24392, #15496, .T. ) ;
#9490=CIRCLE ( 'NONE', #29844, 0.1000000000000000194 ) ;
#9491=EDGE_CURVE ( 'NONE', #23895, #19429, #22286, .T. ) ;
#9493=CARTESIAN_POINT ( 'NONE',  ( -0.3000000000000000999, -2.595429044015121534, -0.5484989581857646623 ) ) ;
#9494=CARTESIAN_POINT ( 'NONE',  ( -0.3000000000000000999, -4.121841830394775030, -0.5449218438908057793 ) ) ;
#9508=ORIENTED_EDGE ( 'NONE', *, *, #17805, .F. ) ;
#9510=AXIS2_PLACEMENT_3D ( 'NONE', #3033, #21558, #34077 ) ;
#9519=CONICAL_SURFACE ( 'NONE', #22024, 0.1600000000000015854, 1.047197551196600296 ) ;
#9523=CARTESIAN_POINT ( 'NONE',  ( -0.3000000000000000999, -3.705001275441084818, -0.3950781284944322458 ) ) ;
#9539=CIRCLE ( 'NONE', #8208, 0.1000000000000000194 ) ;
#9546=AXIS2_PLACEMENT_3D ( 'NONE', #33310, #2048, #18090 ) ;
#9556=EDGE_LOOP ( 'NONE', ( #18930, #21529, #31242, #15603 ) ) ;
#9561=PLANE ( 'NONE',  #3024 ) ;
#9567=ORIENTED_EDGE ( 'NONE', *, *, #25142, .F. ) ;
#9576=DIRECTION ( 'NONE',  ( -0.8660254037844412611, 0.1781528605886697758, 0.4671847153579293810 ) ) ;
#9584=DIRECTION ( 'NONE',  ( 0.000000000000000000, 0.8438867430782092116, 0.5365213554527465956 ) ) ;
#9593=PLANE ( 'NONE',  #37636 ) ;
#9607=CARTESIAN_POINT ( 'NONE',  ( -0.2399999999999999079, -3.478759481804464038, -0.3573324461326447543 ) ) ;
#9613=ORIENTED_EDGE ( 'NONE', *, *, #30340, .T. ) ;
#9656=EDGE_LOOP ( 'NONE', ( #8521, #4448, #26641, #34495 ) ) ;
#9657=CYLINDRICAL_SURFACE ( 'NONE', #34832, 0.1000000000000000056 ) ;
#9664=ORIENTED_EDGE ( 'NONE', *, *, #6230, .F. ) ;
#9666=VERTEX_POINT ( 'NONE', #19997 ) ;
#9676=EDGE_CURVE ( 'NONE', #22855, #19587, #13269, .T. ) ;
#9692=EDGE_CURVE ( 'NONE', #9666, #3317, #10947, .T. ) ;
#9721=DIRECTION ( 'NONE',  ( 1.000000000000000000, 0.000000000000000000, 0.000000000000000000 ) ) ;
#9725=EDGE_LOOP ( 'NONE', ( #14989, #34786, #40622, #24019 ) ) ;
#9786=DIRECTION ( 'NONE',  ( 1.000000000000000000, 0.000000000000000000, 0.000000000000000000 ) ) ;
#9796=ORIENTED_EDGE ( 'NONE', *, *, #14316, .F. ) ;
#9809=VERTEX_POINT ( 'NONE', #36433 ) ;
#9816=ORIENTED_EDGE ( 'NONE', *, *, #5165, .F. ) ;
#9823=CARTESIAN_POINT ( 'NONE',  ( -0.2746410161513776482, -4.385325017590463226, -0.5985264029706663935 ) ) ;
#9850=DIRECTION ( 'NONE',  ( 1.000000000000000000, 0.000000000000000000, 0.000000000000000000 ) ) ;
#9888=CIRCLE ( 'NONE', #21731, 0.09999999999999999167 ) ;
#9893=CARTESIAN_POINT ( 'NONE',  ( -0.3000000000000000999, -3.527715956914472706, -0.3920205355121876289 ) ) ;
#9905=ORIENTED_EDGE ( 'NONE', *, *, #21991, .T. ) ;
#9912=VERTEX_POINT ( 'NONE', #30866 ) ;
#9915=AXIS2_PLACEMENT_3D ( 'NONE', #39649, #5086, #17646 ) ;
#9928=DIRECTION ( 'NONE',  ( 1.000000000000000000, 0.000000000000000000, 0.000000000000000000 ) ) ;
#9934=EDGE_CURVE ( 'NONE', #36123, #25560, #28605, .T. ) ;
#9943=CONICAL_SURFACE ( 'NONE', #4033, 0.1600000000000005029, 1.047197551196598742 ) ;
#9949=PLANE ( 'NONE',  #9475 ) ;
#9950=ORIENTED_EDGE ( 'NONE', *, *, #14984, .F. ) ;
#9963=ORIENTED_EDGE ( 'NONE', *, *, #19848, .T. ) ;
#9982=DIRECTION ( 'NONE',  ( 1.000000000000000000, -0.000000000000000000, -0.000000000000000000 ) ) ;
#9992=LINE ( 'NONE', #31406, #5477 ) ;
#9997=DIRECTION ( 'NONE',  ( 0.000000000000000000, 0.000000000000000000, -1.000000000000000000 ) ) ;
#9999=CIRCLE ( 'NONE', #18546, 0.1000000000000000194 ) ;
#10025=VERTEX_POINT ( 'NONE', #37151 ) ;
#10031=DIRECTION ( 'NONE',  ( 1.000000000000000000, -0.000000000000000000, -0.000000000000000000 ) ) ;
#10039=AXIS2_PLACEMENT_3D ( 'NONE', #13329, #25902, #38420 ) ;
#10047=DIRECTION ( 'NONE',  ( -1.000000000000000000, -0.000000000000000000, -0.000000000000000000 ) ) ;
#10057=EDGE_LOOP ( 'NONE', ( #1843, #34604, #12025, #12430 ) ) ;
#10065=CARTESIAN_POINT ( 'NONE',  ( -0.2399999999999999079, -4.289222312108804225, -0.7308809693675260011 ) ) ;
#10075=DIRECTION ( 'NONE',  ( 1.000000000000000000, -0.000000000000000000, -0.000000000000000000 ) ) ;
#10078=VERTEX_POINT ( 'NONE', #27898 ) ;
#10087=FACE_OUTER_BOUND ( 'NONE', #9656, .T. ) ;
#10093=DIRECTION ( 'NONE',  ( 0.000000000000000000, 0.000000000000000000, -1.000000000000000000 ) ) ;
#10105=DIRECTION ( 'NONE',  ( 0.000000000000000000, 0.7071067811865474617, 0.7071067811865474617 ) ) ;
#10116=EDGE_LOOP ( 'NONE', ( #15547, #31172, #21426, #309, #25095 ) ) ;
#10118=ORIENTED_EDGE ( 'NONE', *, *, #29774, .F. ) ;
#10122=DIRECTION ( 'NONE',  ( 0.000000000000000000, 0.000000000000000000, -1.000000000000000000 ) ) ;
#10125=AXIS2_PLACEMENT_3D ( 'NONE', #5830, #18606, #31165 ) ;
#10136=ADVANCED_FACE ( 'NONE', ( #30022 ), #36175, .T. ) ;
#10152=LINE ( 'NONE', #22722, #20831 ) ;
#10154=VECTOR ( 'NONE', #28914, 39.37007874015748854 ) ;
#10160=DIRECTION ( 'NONE',  ( 0.000000000000000000, -0.8438867430782098777, -0.5365213554527457074 ) ) ;
#10198=PLANE ( 'NONE',  #14825 ) ;
#10220=CARTESIAN_POINT ( 'NONE',  ( -0.2399999999999999079, -3.286568920421631290, -0.5766864829451954222 ) ) ;
#10226=LINE ( 'NONE', #7108, #39142 ) ;
#10232=ORIENTED_EDGE ( 'NONE', *, *, #38128, .T. ) ;
#10233=EDGE_CURVE ( 'NONE', #22378, #27741, #25160, .T. ) ;
#10244=EDGE_LOOP ( 'NONE', ( #16576, #8904, #39416, #32512 ) ) ;
#10266=CARTESIAN_POINT ( 'NONE',  ( -0.2399999999999999079, -2.878813263491020180, -0.3823467908819087602 ) ) ;
#10303=DIRECTION ( 'NONE',  ( 1.000000000000000000, 0.000000000000000000, 0.000000000000000000 ) ) ;
#10306=DIRECTION ( 'NONE',  ( -1.000000000000000000, -0.000000000000000000, -0.000000000000000000 ) ) ;
#10325=EDGE_LOOP ( 'NONE', ( #27988, #19017, #1430, #13447 ) ) ;
#10330=EDGE_LOOP ( 'NONE', ( #3241, #12531, #7323, #13306 ) ) ;
#10361=CARTESIAN_POINT ( 'NONE',  ( -0.3000000000000000999, -2.294529520598973082, -0.6534431116140350104 ) ) ;
#10367=ORIENTED_EDGE ( 'NONE', *, *, #34368, .T. ) ;
#10374=DIRECTION ( 'NONE',  ( 1.000000000000000000, -0.000000000000000000, -0.000000000000000000 ) ) ;
#10421=ORIENTED_EDGE ( 'NONE', *, *, #30870, .F. ) ;
#10447=DIRECTION ( 'NONE',  ( 0.000000000000000000, 0.000000000000000000, 1.000000000000000000 ) ) ;
#10465=VERTEX_POINT ( 'NONE', #15240 ) ;
#10468=ORIENTED_EDGE ( 'NONE', *, *, #24369, .T. ) ;
#10477=EDGE_LOOP ( 'NONE', ( #30200, #27624, #38284, #14382 ) ) ;
#10482=CARTESIAN_POINT ( 'NONE',  ( -0.3000000000000000999, -1.891808285041389093, -0.4498908273618595910 ) ) ;
#10499=EDGE_CURVE ( 'NONE', #23694, #26277, #21220, .T. ) ;
#10505=EDGE_CURVE ( 'NONE', #25709, #20955, #22507, .T. ) ;
#10506=DIRECTION ( 'NONE',  ( -1.000000000000000000, 0.000000000000000000, 0.000000000000000000 ) ) ;
#10512=DIRECTION ( 'NONE',  ( -0.4999999999999957812, -0.3085698060533151876, -0.8091876635195469625 ) ) ;
#10516=DIRECTION ( 'NONE',  ( 1.000000000000000000, 0.000000000000000000, 0.000000000000000000 ) ) ;
#10517=CARTESIAN_POINT ( 'NONE',  ( -0.2399999999999999079, -2.945416957892569521, -0.4639726661791638840 ) ) ;
#10524=EDGE_CURVE ( 'NONE', #34849, #10078, #37601, .T. ) ;
#10548=FACE_OUTER_BOUND ( 'NONE', #11726, .T. ) ;
#10582=CIRCLE ( 'NONE', #11234, 0.09999999999999999167 ) ;
#10592=CIRCLE ( 'NONE', #1433, 0.6115209409081865388 ) ;
#10599=LINE ( 'NONE', #16374, #10154 ) ;
#10609=LINE ( 'NONE', #28923, #9473 ) ;
#10616=LINE ( 'NONE', #7736, #38185 ) ;
#10626=ORIENTED_EDGE ( 'NONE', *, *, #23796, .T. ) ;
#10636=EDGE_CURVE ( 'NONE', #32720, #1199, #12556, .T. ) ;
#10642=DIRECTION ( 'NONE',  ( 0.000000000000000000, 0.5781348229923760629, -0.8159412518334723252 ) ) ;
#10644=AXIS2_PLACEMENT_3D ( 'NONE', #29001, #10306, #29418 ) ;
#10668=VERTEX_POINT ( 'NONE', #34765 ) ;
#10732=ORIENTED_EDGE ( 'NONE', *, *, #30268, .T. ) ;
#10734=EDGE_CURVE ( 'NONE', #14679, #36975, #38216, .T. ) ;
#10760=ADVANCED_FACE ( 'NONE', ( #37606 ), #32345, .F. ) ;
#10762=EDGE_CURVE ( 'NONE', #6555, #23895, #9348, .T. ) ;
#10777=CIRCLE ( 'NONE', #39017, 0.09999999999999996392 ) ;
#10779=AXIS2_PLACEMENT_3D ( 'NONE', #5894, #33682, #8576 ) ;
#10784=ORIENTED_EDGE ( 'NONE', *, *, #2442, .F. ) ;
#10799=CARTESIAN_POINT ( 'NONE',  ( -0.3000000000000000999, -1.804235510932644004, -0.05018601889714981862 ) ) ;
#10820=DIRECTION ( 'NONE',  ( 0.000000000000000000, 0.000000000000000000, -1.000000000000000000 ) ) ;
#10839=AXIS2_PLACEMENT_3D ( 'NONE', #21355, #34487, #31411 ) ;
#10841=CONICAL_SURFACE ( 'NONE', #18707, 0.1600000000000004752, 1.047197551196598519 ) ;
#10847=ORIENTED_EDGE ( 'NONE', *, *, #5721, .T. ) ;
#10850=ORIENTED_EDGE ( 'NONE', *, *, #10762, .F. ) ;
#10852=FACE_OUTER_BOUND ( 'NONE', #6527, .T. ) ;
#10853=LINE ( 'NONE', #30375, #28393 ) ;
#10857=CARTESIAN_POINT ( 'NONE',  ( -0.2746410161513770931, -3.237612445311622622, -0.5419983935656527141 ) ) ;
#10865=DIRECTION ( 'NONE',  ( 0.000000000000000000, 3.414809992080316105E-15, -1.000000000000000000 ) ) ;
#10898=CARTESIAN_POINT ( 'NONE',  ( -0.2399999999999999079, -3.216935334666387813, -0.6321346234654038332 ) ) ;
#10909=DIRECTION ( 'NONE',  ( 1.000000000000000000, -0.000000000000000000, -0.000000000000000000 ) ) ;
#10910=LINE ( 'NONE', #23477, #21176 ) ;
#10911=DIRECTION ( 'NONE',  ( 0.000000000000000000, 0.000000000000000000, -1.000000000000000000 ) ) ;
#10917=LINE ( 'NONE', #26558, #15886 ) ;
#10918=CARTESIAN_POINT ( 'NONE',  ( -0.2746410161513770931, -3.220869926774937664, -0.5656276768926112863 ) ) ;
#10924=EDGE_CURVE ( 'NONE', #39872, #23612, #29734, .T. ) ;
#10933=ADVANCED_FACE ( 'NONE', ( #1222 ), #29987, .T. ) ;
#10935=VERTEX_POINT ( 'NONE', #7551 ) ;
#10941=ORIENTED_EDGE ( 'NONE', *, *, #23821, .F. ) ;
#10944=FACE_OUTER_BOUND ( 'NONE', #21780, .T. ) ;
#10947=LINE ( 'NONE', #36023, #25113 ) ;
#10963=DIRECTION ( 'NONE',  ( -1.000000000000000000, 0.000000000000000000, 0.000000000000000000 ) ) ;
#10967=LENGTH_MEASURE_WITH_UNIT ( LENGTH_MEASURE( 0.02539999999999999897 ), #38919 );
#10983=FACE_OUTER_BOUND ( 'NONE', #4528, .T. ) ;
#11015=CARTESIAN_POINT ( 'NONE',  ( -0.2399999999999999079, -3.941790907013290823, -0.4709369376873030477 ) ) ;
#11022=AXIS2_PLACEMENT_3D ( 'NONE', #20202, #4346, #38899 ) ;
#11051=CYLINDRICAL_SURFACE ( 'NONE', #12284, 0.1000000000000000194 ) ;
#11075=ORIENTED_EDGE ( 'NONE', *, *, #10499, .T. ) ;
#11095=DIRECTION ( 'NONE',  ( 1.000000000000000000, -0.000000000000000000, -0.000000000000000000 ) ) ;
#11106=LINE ( 'NONE', #33105, #25334 ) ;
#11112=CARTESIAN_POINT ( 'NONE',  ( -0.2746410161513776482, -3.880844374714816247, -0.2860650318788287017 ) ) ;
#11125=ORIENTED_EDGE ( 'NONE', *, *, #20791, .F. ) ;
#11141=DIRECTION ( 'NONE',  ( -1.000000000000000000, -0.000000000000000000, -0.000000000000000000 ) ) ;
#11144=CARTESIAN_POINT ( 'NONE',  ( -0.3000000000000000999, -2.322955634169589612, -0.9336221289765171960 ) ) ;
#11149=FACE_BOUND ( 'NONE', #31119, .T. ) ;
#11174=ORIENTED_EDGE ( 'NONE', *, *, #21854, .F. ) ;
#11216=VERTEX_POINT ( 'NONE', #11112 ) ;
#11234=AXIS2_PLACEMENT_3D ( 'NONE', #28228, #15887, #37689 ) ;
#11236=DIRECTION ( 'NONE',  ( 0.000000000000000000, 0.000000000000000000, -1.000000000000000000 ) ) ;
#11241=EDGE_CURVE ( 'NONE', #2621, #8621, #21200, .T. ) ;
#11257=DIRECTION ( 'NONE',  ( 0.000000000000000000, 0.000000000000000000, -1.000000000000000000 ) ) ;
#11258=DIRECTION ( 'NONE',  ( 0.000000000000000000, 0.000000000000000000, 1.000000000000000000 ) ) ;
#11288=EDGE_LOOP ( 'NONE', ( #16373, #39390, #19933, #20712, #17449, #24700, #35668, #1397, #5848 ) ) ;
#11296=CARTESIAN_POINT ( 'NONE',  ( -0.2399999999999999079, -2.416006048095809877, -1.059240699271965402 ) ) ;
#11304=CYLINDRICAL_SURFACE ( 'NONE', #6922, 0.1000000000000000194 ) ;
#11319=DIRECTION ( 'NONE',  ( 0.000000000000000000, 0.000000000000000000, -1.000000000000000000 ) ) ;
#11320=AXIS2_PLACEMENT_3D ( 'NONE', #28405, #24726, #8867 ) ;
#11321=DIRECTION ( 'NONE',  ( 0.000000000000000000, 0.000000000000000000, -1.000000000000000000 ) ) ;
#11336=ORIENTED_EDGE ( 'NONE', *, *, #5471, .T. ) ;
#11343=CARTESIAN_POINT ( 'NONE',  ( -0.2399999999999999079, -2.183180860297908144, -0.4937760292030871079 ) ) ;
#11344=DIRECTION ( 'NONE',  ( 0.4999999999999966693, 0.3120216385968345163, 0.8078629197130845485 ) ) ;
#11350=DIRECTION ( 'NONE',  ( 1.000000000000000000, 0.000000000000000000, 0.000000000000000000 ) ) ;
#11359=AXIS2_PLACEMENT_3D ( 'NONE', #13723, #26289, #10642 ) ;
#11371=CARTESIAN_POINT ( 'NONE',  ( -0.2746410161513770931, -2.853330612949663170, -0.7088139570729240502 ) ) ;
#11375=VERTEX_POINT ( 'NONE', #26760 ) ;
#11386=VECTOR ( 'NONE', #16240, 39.37007874015748143 ) ;
#11397=CIRCLE ( 'NONE', #32407, 0.06250000000000001388 ) ;
#11399=( GEOMETRIC_REPRESENTATION_CONTEXT ( 3 ) GLOBAL_UNCERTAINTY_ASSIGNED_CONTEXT ( ( #15737 ) ) GLOBAL_UNIT_ASSIGNED_CONTEXT ( ( #1126, #26195, #23112 ) ) REPRESENTATION_CONTEXT ( 'NONE', 'WORKASPACE' ) );
#11433=EDGE_CURVE ( 'NONE', #24980, #28467, #8609, .T. ) ;
#11458=EDGE_CURVE ( 'NONE', #24285, #33731, #34540, .T. ) ;
#11471=CARTESIAN_POINT ( 'NONE',  ( -0.2399999999999999079, -2.409101312171279208, -0.6551853038253486750 ) ) ;
#11478=CIRCLE ( 'NONE', #30535, 0.1946589359789743512 ) ;
#11480=ORIENTED_EDGE ( 'NONE', *, *, #19807, .F. ) ;
#11497=ORIENTED_EDGE ( 'NONE', *, *, #1666, .T. ) ;
#11510=EDGE_CURVE ( 'NONE', #25560, #32375, #13989, .T. ) ;
#11527=CARTESIAN_POINT ( 'NONE',  ( -0.2746410161513779258, -2.457388234162025675, -0.5792354969483111127 ) ) ;
#11531=ORIENTED_EDGE ( 'NONE', *, *, #20496, .F. ) ;
#11535=AXIS2_PLACEMENT_3D ( 'NONE', #37909, #9721, #35623 ) ;
#11540=EDGE_LOOP ( 'NONE', ( #5376, #21104, #29479, #11125 ) ) ;
#11551=CARTESIAN_POINT ( 'NONE',  ( -0.2399999999999999079, -3.795222634959446673, 0.02956464416125691164 ) ) ;
#11554=ORIENTED_EDGE ( 'NONE', *, *, #6473, .T. ) ;
#11555=ORIENTED_EDGE ( 'NONE', *, *, #38083, .T. ) ;
#11563=DIRECTION ( 'NONE',  ( 0.000000000000000000, -0.5365213554527478168, 0.8438867430782083234 ) ) ;
#11583=VERTEX_POINT ( 'NONE', #13548 ) ;
#11589=LINE ( 'NONE', #14653, #40160 ) ;
#11592=ORIENTED_EDGE ( 'NONE', *, *, #14683, .T. ) ;
#11593=ORIENTED_EDGE ( 'NONE', *, *, #33873, .T. ) ;
#11601=AXIS2_PLACEMENT_3D ( 'NONE', #26903, #39434, #11257 ) ;
#11605=DIRECTION ( 'NONE',  ( 0.000000000000000000, 0.000000000000000000, 1.000000000000000000 ) ) ;
#11611=CARTESIAN_POINT ( 'NONE',  ( -0.2399999999999999079, -3.285933380171606188, -0.6294744526254046901 ) ) ;
#11617=ADVANCED_FACE ( 'NONE', ( #825 ), #29175, .F. ) ;
#11625=CIRCLE ( 'NONE', #32644, 0.5515209409081861525 ) ;
#11635=VERTEX_POINT ( 'NONE', #233 ) ;
#11681=EDGE_CURVE ( 'NONE', #7026, #4884, #3475, .T. ) ;
#11690=ORIENTED_EDGE ( 'NONE', *, *, #35806, .F. ) ;
#11712=CARTESIAN_POINT ( 'NONE',  ( -0.2746410161513779258, -3.941790907013290823, 0.1405840032208834911 ) ) ;
#11722=CARTESIAN_POINT ( 'NONE',  ( -0.2399999999999999079, -2.853330612949663170, -0.7688139570729241035 ) ) ;
#11726=EDGE_LOOP ( 'NONE', ( #36015, #21000, #37913, #3188 ) ) ;
#11732=VERTEX_POINT ( 'NONE', #32241 ) ;
#11744=ORIENTED_EDGE ( 'NONE', *, *, #5903, .T. ) ;
#11767=DIRECTION ( 'NONE',  ( 1.000000000000000000, 0.000000000000000000, 0.000000000000000000 ) ) ;
#11770=ORIENTED_EDGE ( 'NONE', *, *, #25390, .F. ) ;
#11781=VERTEX_POINT ( 'NONE', #20331 ) ;
#11796=ORIENTED_EDGE ( 'NONE', *, *, #7930, .T. ) ;
#11812=ORIENTED_EDGE ( 'NONE', *, *, #31189, .F. ) ;
#11815=CARTESIAN_POINT ( 'NONE',  ( -0.2399999999999999079, -3.904891172116972786, -0.3813182129431079148 ) ) ;
#11833=CARTESIAN_POINT ( 'NONE',  ( -0.3000000000000000999, -3.335205990917129881, -0.4042613180508735082 ) ) ;
#11837=FACE_OUTER_BOUND ( 'NONE', #29789, .T. ) ;
#11847=FACE_OUTER_BOUND ( 'NONE', #26699, .T. ) ;
#11849=AXIS2_PLACEMENT_3D ( 'NONE', #32461, #33074, #7966 ) ;
#11853=AXIS2_PLACEMENT_3D ( 'NONE', #4935, #20995, #5132 ) ;
#11858=CARTESIAN_POINT ( 'NONE',  ( -0.2399999999999999079, -4.176085227118957022, -0.6840180543573738392 ) ) ;
#11861=CARTESIAN_POINT ( 'NONE',  ( -0.2746410161513779258, -4.320736256378554963, -0.8145269479932405465 ) ) ;
#11878=EDGE_CURVE ( 'NONE', #22635, #36573, #2614, .T. ) ;
#11891=VERTEX_POINT ( 'NONE', #21556 ) ;
#11896=DIRECTION ( 'NONE',  ( -0.000000000000000000, 0.8159412518334716591, 0.5781348229923772841 ) ) ;
#11898=PLANE ( 'NONE',  #29709 ) ;
#11899=CARTESIAN_POINT ( 'NONE',  ( -0.2746410161513770931, -2.891403747035983240, -0.7012825271972917829 ) ) ;
#11902=CARTESIAN_POINT ( 'NONE',  ( -0.3000000000000000999, -2.183180860297908144, -0.4312760292030870524 ) ) ;
#11913=AXIS2_PLACEMENT_3D ( 'NONE', #40007, #20913, #27288 ) ;
#11914=VECTOR ( 'NONE', #17286, 39.37007874015748143 ) ;
#11919=CARTESIAN_POINT ( 'NONE',  ( -0.2746410161513779258, -3.334889855281614857, -0.6641625420049475093 ) ) ;
#11925=DIRECTION ( 'NONE',  ( 0.000000000000000000, 0.000000000000000000, -1.000000000000000000 ) ) ;
#11939=CIRCLE ( 'NONE', #34935, 0.1600000000000004752 ) ;
#11942=ORIENTED_EDGE ( 'NONE', *, *, #26532, .T. ) ;
#11943=EDGE_CURVE ( 'NONE', #13608, #25709, #13357, .T. ) ;
#11971=AXIS2_PLACEMENT_3D ( 'NONE', #21444, #5775, #30876 ) ;
#11978=VECTOR ( 'NONE', #34036, 39.37007874015748143 ) ;
#11986=EDGE_CURVE ( 'NONE', #17567, #2349, #32400, .T. ) ;
#11992=EDGE_CURVE ( 'NONE', #2621, #34142, #40460, .T. ) ;
#12002=CIRCLE ( 'NONE', #4088, 0.1000000000000000194 ) ;
#12020=ADVANCED_FACE ( 'NONE', ( #37364 ), #14671, .T. ) ;
#12025=ORIENTED_EDGE ( 'NONE', *, *, #17073, .F. ) ;
#12042=EDGE_CURVE ( 'NONE', #8991, #10935, #5431, .T. ) ;
#12084=CYLINDRICAL_SURFACE ( 'NONE', #27815, 0.1000000000000000194 ) ;
#12092=CARTESIAN_POINT ( 'NONE',  ( -0.2746410161513779258, -1.804235510932644004, -0.1501860188971498311 ) ) ;
#12100=AXIS2_PLACEMENT_3D ( 'NONE', #34691, #3821, #6497 ) ;
#12108=VERTEX_POINT ( 'NONE', #22360 ) ;
#12115=CIRCLE ( 'NONE', #4860, 0.1000000000000000194 ) ;
#12118=DIRECTION ( 'NONE',  ( -0.000000000000000000, 0.5781348229923771731, -0.8159412518334715481 ) ) ;
#12126=DIRECTION ( 'NONE',  ( -0.000000000000000000, -0.7071067811865473507, -0.7071067811865475727 ) ) ;
#12151=LINE ( 'NONE', #14612, #34489 ) ;
#12183=DIRECTION ( 'NONE',  ( 0.000000000000000000, -3.414809992080316105E-15, -1.000000000000000000 ) ) ;
#12187=EDGE_LOOP ( 'NONE', ( #20661, #32531, #35678, #20599 ) ) ;
#12193=ORIENTED_EDGE ( 'NONE', *, *, #32337, .T. ) ;
#12201=CARTESIAN_POINT ( 'NONE',  ( -0.2746410161513776482, -3.672249662662566472, -0.1880352225538197142 ) ) ;
#12209=LINE ( 'NONE', #14888, #32918 ) ;
#12233=ORIENTED_EDGE ( 'NONE', *, *, #37908, .T. ) ;
#12237=ORIENTED_EDGE ( 'NONE', *, *, #17031, .T. ) ;
#12279=ADVANCED_FACE ( 'NONE', ( #35482 ), #1182, .T. ) ;
#12284=AXIS2_PLACEMENT_3D ( 'NONE', #38796, #36327, #11236 ) ;
#12303=ORIENTED_EDGE ( 'NONE', *, *, #6586, .T. ) ;
#12319=VERTEX_POINT ( 'NONE', #24793 ) ;
#12344=CARTESIAN_POINT ( 'NONE',  ( -0.2746410161513776482, -3.811657270145150989, -0.1642545796697100491 ) ) ;
#12369=DIRECTION ( 'NONE',  ( 0.000000000000000000, 0.000000000000000000, -1.000000000000000000 ) ) ;
#12371=CYLINDRICAL_SURFACE ( 'NONE', #21345, 0.1000000000000000194 ) ;
#12377=DIRECTION ( 'NONE',  ( 0.000000000000000000, 0.000000000000000000, 1.000000000000000000 ) ) ;
#12380=CARTESIAN_POINT ( 'NONE',  ( -0.2746410161513770931, -3.335205990917129881, -0.4042613180508733972 ) ) ;
#12382=DIRECTION ( 'NONE',  ( -1.000000000000000000, -0.000000000000000000, -0.000000000000000000 ) ) ;
#12388=ORIENTED_EDGE ( 'NONE', *, *, #10524, .F. ) ;
#12392=DIRECTION ( 'NONE',  ( 0.000000000000000000, -0.5781348229923760629, 0.8159412518334723252 ) ) ;
#12404=ORIENTED_EDGE ( 'NONE', *, *, #14224, .F. ) ;
#12413=DIRECTION ( 'NONE',  ( 1.000000000000000000, 0.000000000000000000, 0.000000000000000000 ) ) ;
#12418=ADVANCED_FACE ( 'NONE', ( #38531 ), #16936, .F. ) ;
#12430=ORIENTED_EDGE ( 'NONE', *, *, #14188, .F. ) ;
#12435=PLANE ( 'NONE',  #31197 ) ;
#12444=LINE ( 'NONE', #40217, #2675 ) ;
#12475=ORIENTED_EDGE ( 'NONE', *, *, #3848, .T. ) ;
#12478=LINE ( 'NONE', #10220, #24973 ) ;
#12489=EDGE_LOOP ( 'NONE', ( #27484, #15497, #29800, #12750 ) ) ;
#12499=ORIENTED_EDGE ( 'NONE', *, *, #30840, .T. ) ;
#12507=PLANE ( 'NONE',  #13228 ) ;
#12531=ORIENTED_EDGE ( 'NONE', *, *, #23159, .F. ) ;
#12532=VERTEX_POINT ( 'NONE', #8885 ) ;
#12537=AXIS2_PLACEMENT_3D ( 'NONE', #17961, #39775, #11605 ) ;
#12547=EDGE_CURVE ( 'NONE', #20195, #10465, #17549, .T. ) ;
#12550=ORIENTED_EDGE ( 'NONE', *, *, #18803, .F. ) ;
#12556=LINE ( 'NONE', #19150, #38255 ) ;
#12568=FACE_OUTER_BOUND ( 'NONE', #6567, .T. ) ;
#12594=CARTESIAN_POINT ( 'NONE',  ( -0.2399999999999999079, -2.511040369707300268, -0.5948468226404902692 ) ) ;
#12602=ORIENTED_EDGE ( 'NONE', *, *, #31760, .F. ) ;
#12616=LINE ( 'NONE', #19010, #1142 ) ;
#12619=CARTESIAN_POINT ( 'NONE',  ( -0.3000000000000000999, -3.840189043187996809, -0.1239867222638698224 ) ) ;
#12620=CARTESIAN_POINT ( 'NONE',  ( -0.2399999999999999079, -3.941790907013290823, -0.4709369376873030477 ) ) ;
#12626=ORIENTED_EDGE ( 'NONE', *, *, #11986, .T. ) ;
#12627=CARTESIAN_POINT ( 'NONE',  ( -0.2399999999999999079, -3.941790907013290823, -0.4709369376873030477 ) ) ;
#12628=ORIENTED_EDGE ( 'NONE', *, *, #26817, .T. ) ;
#12632=DIRECTION ( 'NONE',  ( -0.4709550870498624975, 0.000000000000000000, 0.8821571889305536152 ) ) ;
#12634=ORIENTED_EDGE ( 'NONE', *, *, #28363, .F. ) ;
#12666=DIRECTION ( 'NONE',  ( 0.000000000000000000, 0.000000000000000000, -1.000000000000000000 ) ) ;
#12669=VECTOR ( 'NONE', #34383, 39.37007874015748854 ) ;
#12688=DIRECTION ( 'NONE',  ( 0.000000000000000000, -0.5781348229923758408, 0.8159412518334724362 ) ) ;
#12691=VERTEX_POINT ( 'NONE', #28215 ) ;
#12694=EDGE_LOOP ( 'NONE', ( #15597, #7900, #11531, #16479 ) ) ;
#12703=EDGE_LOOP ( 'NONE', ( #43, #15218, #35484, #17799 ) ) ;
#12709=CARTESIAN_POINT ( 'NONE',  ( -0.2399999999999999079, -2.599675038826658735, -0.8213992999509311943 ) ) ;
#12718=CARTESIAN_POINT ( 'NONE',  ( -0.2746410161513776482, -3.730063144961804245, -0.1064410973704723457 ) ) ;
#12750=ORIENTED_EDGE ( 'NONE', *, *, #8917, .F. ) ;
#12767=PLANE ( 'NONE',  #24032 ) ;
#12777=DIRECTION ( 'NONE',  ( 1.000000000000000000, 0.000000000000000000, 0.000000000000000000 ) ) ;
#12786=AXIS2_PLACEMENT_3D ( 'NONE', #1913, #2097, #29472 ) ;
#12802=VERTEX_POINT ( 'NONE', #17040 ) ;
#12824=EDGE_LOOP ( 'NONE', ( #8847, #27449, #32714, #910, #20969, #25707, #34443, #36055, #10847, #13753, #11555, #29488, #11593, #39103, #28636, #40277, #15211, #38787, #24677, #18969, #18654, #39271, #21658, #23682, #18694, #1258, #11497 ) ) ;
#12845=ORIENTED_EDGE ( 'NONE', *, *, #39807, .T. ) ;
#12850=DIRECTION ( 'NONE',  ( -1.000000000000000000, -0.000000000000000000, -0.000000000000000000 ) ) ;
#12854=DIRECTION ( 'NONE',  ( 0.000000000000000000, 0.000000000000000000, 1.000000000000000000 ) ) ;
#12857=EDGE_LOOP ( 'NONE', ( #28123, #6366, #2450, #39005 ) ) ;
#12888=DIRECTION ( 'NONE',  ( 0.000000000000000000, 0.000000000000000000, -1.000000000000000000 ) ) ;
#12897=LINE ( 'NONE', #28524, #35588 ) ;
#12906=CARTESIAN_POINT ( 'NONE',  ( -0.2399999999999999079, -3.220869926774937664, -0.5656276768926112863 ) ) ;
#12919=CONICAL_SURFACE ( 'NONE', #8939, 0.1600000000000015854, 1.047197551196600296 ) ;
#12933=CARTESIAN_POINT ( 'NONE',  ( -0.2399999999999999079, -1.835749455202394298, -0.3938319975228649072 ) ) ;
#12954=ORIENTED_EDGE ( 'NONE', *, *, #24940, .T. ) ;
#12955=CIRCLE ( 'NONE', #6357, 0.1000000000000000194 ) ;
#12957=LINE ( 'NONE', #37624, #9204 ) ;
#12981=DIRECTION ( 'NONE',  ( 0.000000000000000000, 0.000000000000000000, 1.000000000000000000 ) ) ;
#13007=ORIENTED_EDGE ( 'NONE', *, *, #13158, .T. ) ;
#13014=CARTESIAN_POINT ( 'NONE',  ( -0.3000000000000000999, -3.609310082097819894, -0.4498340178114252352 ) ) ;
#13018=ADVANCED_FACE ( 'NONE', ( #22178 ), #29836, .F. ) ;
#13039=EDGE_CURVE ( 'NONE', #34047, #3165, #38379, .T. ) ;
#13045=CARTESIAN_POINT ( 'NONE',  ( -0.2399999999999999079, -2.778907721888695281, -0.2599079779360263798 ) ) ;
#13046=ORIENTED_EDGE ( 'NONE', *, *, #22888, .F. ) ;
#13056=FACE_OUTER_BOUND ( 'NONE', #22779, .T. ) ;
#13075=CARTESIAN_POINT ( 'NONE',  ( -0.2746410161513776482, -4.233163482269810096, -0.5148221395285308422 ) ) ;
#13096=DIRECTION ( 'NONE',  ( 0.000000000000000000, 0.000000000000000000, -1.000000000000000000 ) ) ;
#13114=PLANE ( 'NONE',  #36222 ) ;
#13119=CARTESIAN_POINT ( 'NONE',  ( -0.2399999999999999079, -2.163125352510477661, -0.3606189578686002095 ) ) ;
#13125=DIRECTION ( 'NONE',  ( -1.000000000000000000, -0.000000000000000000, -0.000000000000000000 ) ) ;
#13131=CARTESIAN_POINT ( 'NONE',  ( -0.2399999999999999079, -3.757033409510397881, -0.3216434158294207424 ) ) ;
#13133=EDGE_LOOP ( 'NONE', ( #37472, #22894, #4120, #35725, #4071, #14211, #15027, #22281, #13292, #4201, #38286, #4190 ) ) ;
#13135=ORIENTED_EDGE ( 'NONE', *, *, #31928, .F. ) ;
#13136=CARTESIAN_POINT ( 'NONE',  ( -0.3000000000000000999, -3.723902497147952406, 0.1004495357399106253 ) ) ;
#13145=AXIS2_PLACEMENT_3D ( 'NONE', #12620, #31755, #25183 ) ;
#13152=EDGE_LOOP ( 'NONE', ( #18395, #38240, #36694, #33444 ) ) ;
#13158=EDGE_CURVE ( 'NONE', #14891, #8015, #10777, .T. ) ;
#13175=CIRCLE ( 'NONE', #8590, 0.1946589359789743512 ) ;
#13177=FACE_OUTER_BOUND ( 'NONE', #13183, .T. ) ;
#13181=ORIENTED_EDGE ( 'NONE', *, *, #15256, .T. ) ;
#13183=EDGE_LOOP ( 'NONE', ( #23940, #24353, #467, #28140 ) ) ;
#13219=CARTESIAN_POINT ( 'NONE',  ( -0.2746410161513776482, -4.134278792318540674, -0.4999285807449073693 ) ) ;
#13225=CARTESIAN_POINT ( 'NONE',  ( -0.2746410161513779258, -2.183180860297908144, -0.4937760292030871079 ) ) ;
#13228=AXIS2_PLACEMENT_3D ( 'NONE', #16404, #15797, #34923 ) ;
#13238=ADVANCED_FACE ( 'NONE', ( #16796 ), #33424, .T. ) ;
#13239=CARTESIAN_POINT ( 'NONE',  ( -0.2399999999999999079, -3.838583118162426810, -0.3058907208964237734 ) ) ;
#13246=LINE ( 'NONE', #35048, #7343 ) ;
#13249=EDGE_CURVE ( 'NONE', #15800, #31618, #40609, .T. ) ;
#13251=CYLINDRICAL_SURFACE ( 'NONE', #6637, 0.1000000000000000056 ) ;
#13263=EDGE_LOOP ( 'NONE', ( #6039, #36988, #5607, #32591 ) ) ;
#13269=CIRCLE ( 'NONE', #27717, 0.1000000000000000194 ) ;
#13288=EDGE_CURVE ( 'NONE', #12319, #11781, #14709, .T. ) ;
#13289=CYLINDRICAL_SURFACE ( 'NONE', #28371, 0.4615209409081865166 ) ;
#13292=ORIENTED_EDGE ( 'NONE', *, *, #34083, .T. ) ;
#13297=CARTESIAN_POINT ( 'NONE',  ( -0.3000000000000000999, -3.941790907013290823, -0.4709369376873030477 ) ) ;
#13306=ORIENTED_EDGE ( 'NONE', *, *, #32828, .F. ) ;
#13308=DIRECTION ( 'NONE',  ( -1.000000000000000000, -0.000000000000000000, -0.000000000000000000 ) ) ;
#13328=FACE_OUTER_BOUND ( 'NONE', #39860, .T. ) ;
#13329=CARTESIAN_POINT ( 'NONE',  ( -0.3000000000000000999, -2.511040369707300268, -0.4948468226404901804 ) ) ;
#13335=DIRECTION ( 'NONE',  ( -1.000000000000000000, -0.000000000000000000, -0.000000000000000000 ) ) ;
#13342=LINE ( 'NONE', #13131, #7876 ) ;
#13357=CIRCLE ( 'NONE', #25854, 0.1600000000000015854 ) ;
#13359=AXIS2_PLACEMENT_3D ( 'NONE', #27163, #8614, #27764 ) ;
#13374=EDGE_CURVE ( 'NONE', #20247, #24904, #21980, .T. ) ;
#13379=DIRECTION ( 'NONE',  ( -1.000000000000000000, -0.000000000000000000, -0.000000000000000000 ) ) ;
#13388=CARTESIAN_POINT ( 'NONE',  ( -0.3000000000000000999, -2.909786385774835171, -0.3705357231075771529 ) ) ;
#13392=CIRCLE ( 'NONE', #35095, 0.1000000000000000194 ) ;
#13400=ORIENTED_EDGE ( 'NONE', *, *, #40185, .T. ) ;
#13404=ORIENTED_EDGE ( 'NONE', *, *, #11986, .F. ) ;
#13417=EDGE_CURVE ( 'NONE', #20195, #2786, #18391, .T. ) ;
#13432=DIRECTION ( 'NONE',  ( -0.4999999999999986677, 0.000000000000000000, 0.8660254037844393737 ) ) ;
#13435=ADVANCED_FACE ( 'NONE', ( #3364 ), #37936, .F. ) ;
#13439=DIRECTION ( 'NONE',  ( -1.000000000000000000, 0.000000000000000000, 0.000000000000000000 ) ) ;
#13440=VECTOR ( 'NONE', #20658, 39.37007874015748854 ) ;
#13442=CARTESIAN_POINT ( 'NONE',  ( -0.2399999999999999079, -2.317513802384189692, -0.4844117508308344866 ) ) ;
#13446=ADVANCED_FACE ( 'NONE', ( #38125 ), #9949, .T. ) ;
#13447=ORIENTED_EDGE ( 'NONE', *, *, #40185, .F. ) ;
#13462=CARTESIAN_POINT ( 'NONE',  ( -0.2746410161513782033, -1.835749455202394298, -0.3938319975228649072 ) ) ;
#13498=CARTESIAN_POINT ( 'NONE',  ( -0.2399999999999999079, -2.416006048095809877, -1.059240699271965402 ) ) ;
#13534=ADVANCED_FACE ( 'NONE', ( #10983 ), #1327, .F. ) ;
#13548=CARTESIAN_POINT ( 'NONE',  ( -0.3000000000000000999, -3.758594918004649621, -0.06617323996463192470 ) ) ;
#13557=ORIENTED_EDGE ( 'NONE', *, *, #10233, .F. ) ;
#13558=EDGE_CURVE ( 'NONE', #36582, #4130, #35444, .T. ) ;
#13575=CARTESIAN_POINT ( 'NONE',  ( -0.2399999999999999079, -1.891808285041389093, -0.4498908273618595910 ) ) ;
#13578=EDGE_LOOP ( 'NONE', ( #35820, #15425, #26058, #23044, #28276 ) ) ;
#13590=DIRECTION ( 'NONE',  ( 1.000000000000000000, -0.000000000000000000, -0.000000000000000000 ) ) ;
#13603=ORIENTED_EDGE ( 'NONE', *, *, #2706, .F. ) ;
#13604=CYLINDRICAL_SURFACE ( 'NONE', #5262, 0.1000000000000000194 ) ;
#13607=EDGE_LOOP ( 'NONE', ( #27791, #20278, #7171, #10118 ) ) ;
#13608=VERTEX_POINT ( 'NONE', #2331 ) ;
#13609=ORIENTED_EDGE ( 'NONE', *, *, #8114, .T. ) ;
#13634=SHAPE_DEFINITION_REPRESENTATION ( #22606, #21742 ) ;
#13644=ADVANCED_FACE ( 'NONE', ( #26755 ), #23056, .F. ) ;
#13647=ORIENTED_EDGE ( 'NONE', *, *, #30157, .F. ) ;
#13667=EDGE_CURVE ( 'NONE', #38406, #28968, #13775, .T. ) ;
#13710=DIRECTION ( 'NONE',  ( 0.000000000000000000, -0.9343694307158671997, 0.3563057211773427713 ) ) ;
#13722=DIRECTION ( 'NONE',  ( 1.000000000000000000, -0.000000000000000000, -0.000000000000000000 ) ) ;
#13723=CARTESIAN_POINT ( 'NONE',  ( -0.2399999999999999079, -3.672249662662566472, -0.1880352225538197142 ) ) ;
#13728=FACE_OUTER_BOUND ( 'NONE', #12489, .T. ) ;
#13753=ORIENTED_EDGE ( 'NONE', *, *, #35811, .T. ) ;
#13761=CARTESIAN_POINT ( 'NONE',  ( -0.2746410161513770931, -2.878813263491020180, -0.3823467908819087602 ) ) ;
#13775=LINE ( 'NONE', #1463, #31833 ) ;
#13799=CARTESIAN_POINT ( 'NONE',  ( -0.2399999999999999079, -2.026158573466833257, -0.3155405389364156488 ) ) ;
#13830=ORIENTED_EDGE ( 'NONE', *, *, #22110, .T. ) ;
#13836=DIRECTION ( 'NONE',  ( 1.000000000000000000, 0.000000000000000000, 0.000000000000000000 ) ) ;
#13847=DIRECTION ( 'NONE',  ( 1.000000000000000000, -0.000000000000000000, -0.000000000000000000 ) ) ;
#13901=CARTESIAN_POINT ( 'NONE',  ( -0.2746410161513776482, -3.941790907013290823, -0.4709369376873030477 ) ) ;
#13922=AXIS2_PLACEMENT_3D ( 'NONE', #16067, #3903, #12981 ) ;
#13945=ORIENTED_EDGE ( 'NONE', *, *, #29097, .F. ) ;
#13964=DIRECTION ( 'NONE',  ( -0.3779644730092268090, 0.000000000000000000, 0.9258200997725516412 ) ) ;
#13973=DIRECTION ( 'NONE',  ( 0.000000000000000000, 0.000000000000000000, -1.000000000000000000 ) ) ;
#13984=CARTESIAN_POINT ( 'NONE',  ( -0.3000000000000000999, -3.880844374714816247, -0.2860650318788287017 ) ) ;
#13988=EDGE_LOOP ( 'NONE', ( #13135, #32168, #32468, #18007 ) ) ;
#13989=CIRCLE ( 'NONE', #8731, 0.1599999999999999201 ) ;
#13992=ADVANCED_FACE ( 'NONE', ( #5695 ), #8992, .F. ) ;
#13996=EDGE_CURVE ( 'NONE', #18456, #11375, #23976, .T. ) ;
#14007=DIRECTION ( 'NONE',  ( -0.8660254037844421493, -0.1903656704315992709, -0.4623428506218321132 ) ) ;
#14022=DIRECTION ( 'NONE',  ( 1.000000000000000000, 0.000000000000000000, 0.000000000000000000 ) ) ;
#14064=VERTEX_POINT ( 'NONE', #3415 ) ;
#14067=VECTOR ( 'NONE', #27900, 39.37007874015748143 ) ;
#14077=DIRECTION ( 'NONE',  ( 0.000000000000000000, 0.000000000000000000, -1.000000000000000000 ) ) ;
#14082=FACE_OUTER_BOUND ( 'NONE', #34572, .T. ) ;
#14090=VERTEX_POINT ( 'NONE', #21961 ) ;
#14092=CARTESIAN_POINT ( 'NONE',  ( -0.2399999999999999079, -3.579933075828130473, -0.2145427270617870641 ) ) ;
#14099=DIRECTION ( 'NONE',  ( -1.000000000000000000, -0.000000000000000000, -0.000000000000000000 ) ) ;
#14108=EDGE_CURVE ( 'NONE', #9912, #35757, #32490, .T. ) ;
#14115=EDGE_LOOP ( 'NONE', ( #15, #28784, #38037, #30231 ) ) ;
#14118=AXIS2_PLACEMENT_3D ( 'NONE', #5334, #39711, #17896 ) ;
#14129=VECTOR ( 'NONE', #39676, 39.37007874015748143 ) ;
#14140=CIRCLE ( 'NONE', #23397, 0.1946589359789743512 ) ;
#14170=DIRECTION ( 'NONE',  ( 0.000000000000000000, -1.024442997624094674E-14, -1.000000000000000000 ) ) ;
#14172=EDGE_CURVE ( 'NONE', #6555, #40516, #10599, .T. ) ;
#14174=ORIENTED_EDGE ( 'NONE', *, *, #1522, .F. ) ;
#14178=FACE_OUTER_BOUND ( 'NONE', #4577, .T. ) ;
#14186=DIRECTION ( 'NONE',  ( 0.000000000000000000, -3.414809992080327938E-15, -1.000000000000000000 ) ) ;
#14188=EDGE_CURVE ( 'NONE', #32592, #15505, #15415, .T. ) ;
#14194=DIRECTION ( 'NONE',  ( 1.000000000000000000, 0.000000000000000000, 0.000000000000000000 ) ) ;
#14211=ORIENTED_EDGE ( 'NONE', *, *, #6354, .T. ) ;
#14224=EDGE_CURVE ( 'NONE', #36975, #12802, #37111, .T. ) ;
#14248=ORIENTED_EDGE ( 'NONE', *, *, #676, .T. ) ;
#14257=AXIS2_PLACEMENT_3D ( 'NONE', #35597, #3919, #10105 ) ;
#14265=DIRECTION ( 'NONE',  ( -1.000000000000000000, 0.000000000000000000, 0.000000000000000000 ) ) ;
#14289=CARTESIAN_POINT ( 'NONE',  ( -0.2399999999999999079, -1.804235510932644004, -0.1501860188971498311 ) ) ;
#14310=ADVANCED_FACE ( 'NONE', ( #32200 ), #4014, .F. ) ;
#14316=EDGE_CURVE ( 'NONE', #9001, #21617, #9539, .T. ) ;
#14317=LINE ( 'NONE', #35501, #17163 ) ;
#14318=ORIENTED_EDGE ( 'NONE', *, *, #22230, .T. ) ;
#14323=VERTEX_POINT ( 'NONE', #23392 ) ;
#14341=DIRECTION ( 'NONE',  ( -1.000000000000000000, -0.000000000000000000, -0.000000000000000000 ) ) ;
#14374=CARTESIAN_POINT ( 'NONE',  ( -0.2746410161513782033, -2.292669950144801572, -0.8383185228372386222 ) ) ;
#14381=DIRECTION ( 'NONE',  ( 1.000000000000000000, -0.000000000000000000, -0.000000000000000000 ) ) ;
#14382=ORIENTED_EDGE ( 'NONE', *, *, #18213, .F. ) ;
#14398=ORIENTED_EDGE ( 'NONE', *, *, #39807, .F. ) ;
#14455=EDGE_LOOP ( 'NONE', ( #36631, #9231, #40112, #1800 ) ) ;
#14456=CARTESIAN_POINT ( 'NONE',  ( -0.2399999999999999079, -3.849534981189179028, -0.3510928155360652503 ) ) ;
#14460=CONICAL_SURFACE ( 'NONE', #38767, 0.4615209409081865166, 1.047197551196599852 ) ;
#14469=CARTESIAN_POINT ( 'NONE',  ( -0.2399999999999999079, -3.253295730098268113, -0.6063490597057096254 ) ) ;
#14471=CARTESIAN_POINT ( 'NONE',  ( -0.2399999999999999079, -3.961846414800720861, -0.6040940090217902236 ) ) ;
#14472=DIRECTION ( 'NONE',  ( -1.000000000000000000, -0.000000000000000000, -0.000000000000000000 ) ) ;
#14504=CARTESIAN_POINT ( 'NONE',  ( -0.2746410161513779258, -3.985676108854518507, -0.6623095129438225648 ) ) ;
#14517=FACE_OUTER_BOUND ( 'NONE', #10057, .T. ) ;
#14523=AXIS2_PLACEMENT_3D ( 'NONE', #22182, #3640, #31611 ) ;
#14539=EDGE_CURVE ( 'NONE', #11583, #15927, #20713, .T. ) ;
#14597=EDGE_LOOP ( 'NONE', ( #38798, #38368, #10421, #22992 ) ) ;
#14605=AXIS2_PLACEMENT_3D ( 'NONE', #28771, #630, #817 ) ;
#14612=CARTESIAN_POINT ( 'NONE',  ( -0.2399999999999999079, -2.289343986263487896, -0.6686455968847019316 ) ) ;
#14625=CARTESIAN_POINT ( 'NONE',  ( -0.2746410161513776482, -3.753843787845913216, -0.2458487048530572650 ) ) ;
#14632=DIRECTION ( 'NONE',  ( 0.000000000000000000, -0.5781348229923760629, 0.8159412518334724362 ) ) ;
#14647=CARTESIAN_POINT ( 'NONE',  ( -0.3000000000000000999, -3.941790907013290823, -0.4709369376873030477 ) ) ;
#14653=CARTESIAN_POINT ( 'NONE',  ( -0.2746410161513770931, -3.525450504378606187, -0.1357627943591874498 ) ) ;
#14662=CARTESIAN_POINT ( 'NONE',  ( -0.2399999999999999079, -2.809880844172510272, -0.2480969101616946337 ) ) ;
#14665=DIRECTION ( 'NONE',  ( 0.000000000000000000, 0.8438867430782092116, 0.5365213554527465956 ) ) ;
#14671=CONICAL_SURFACE ( 'NONE', #19938, 0.1946589359789743512, 1.047197551196599186 ) ;
#14679=VERTEX_POINT ( 'NONE', #35256 ) ;
#14683=EDGE_CURVE ( 'NONE', #9809, #33422, #16334, .T. ) ;
#14687=CYLINDRICAL_SURFACE ( 'NONE', #20591, 0.1000000000000000194 ) ;
#14699=VECTOR ( 'NONE', #32628, 39.37007874015748143 ) ;
#14709=LINE ( 'NONE', #21694, #31801 ) ;
#14710=EDGE_CURVE ( 'NONE', #34890, #35716, #6441, .T. ) ;
#14725=ORIENTED_EDGE ( 'NONE', *, *, #6473, .F. ) ;
#14750=AXIS2_PLACEMENT_3D ( 'NONE', #7382, #4703, #14186 ) ;
#14759=DIRECTION ( 'NONE',  ( 0.4999999999999978351, -0.8322738431953016214, -0.2394164779895580630 ) ) ;
#14767=VERTEX_POINT ( 'NONE', #23721 ) ;
#14769=CIRCLE ( 'NONE', #15416, 0.5215209409081880132 ) ;
#14797=CIRCLE ( 'NONE', #38424, 0.09999999999999996392 ) ;
#14798=VECTOR ( 'NONE', #3967, 39.37007874015748854 ) ;
#14813=DIRECTION ( 'NONE',  ( -1.000000000000000000, -0.000000000000000000, -0.000000000000000000 ) ) ;
#14818=ORIENTED_EDGE ( 'NONE', *, *, #31189, .T. ) ;
#14821=PLANE ( 'NONE',  #11853 ) ;
#14825=AXIS2_PLACEMENT_3D ( 'NONE', #31996, #16363, #9584 ) ;
#14873=ORIENTED_EDGE ( 'NONE', *, *, #17074, .F. ) ;
#14881=PLANE ( 'NONE',  #36226 ) ;
#14888=CARTESIAN_POINT ( 'NONE',  ( -0.2399999999999999079, -4.056386786973173564, -0.6915988348251679296 ) ) ;
#14891=VERTEX_POINT ( 'NONE', #27822 ) ;
#14892=EDGE_LOOP ( 'NONE', ( #28386, #9613, #35657, #15036 ) ) ;
#14893=FACE_OUTER_BOUND ( 'NONE', #2038, .T. ) ;
#14903=DIRECTION ( 'NONE',  ( 0.000000000000000000, 0.000000000000000000, -1.000000000000000000 ) ) ;
#14911=VERTEX_POINT ( 'NONE', #31323 ) ;
#14935=DIRECTION ( 'NONE',  ( 1.000000000000000000, -0.000000000000000000, -0.000000000000000000 ) ) ;
#14949=DIRECTION ( 'NONE',  ( -1.000000000000000000, 0.000000000000000000, 0.000000000000000000 ) ) ;
#14956=LINE ( 'NONE', #11471, #4361 ) ;
#14958=CARTESIAN_POINT ( 'NONE',  ( -0.2746410161513776482, -3.941790907013290823, -0.4709369376873030477 ) ) ;
#14968=ORIENTED_EDGE ( 'NONE', *, *, #7672, .F. ) ;
#14970=CYLINDRICAL_SURFACE ( 'NONE', #19090, 0.1000000000000000194 ) ;
#14980=CARTESIAN_POINT ( 'NONE',  ( -0.2399999999999999079, -2.253314830856113726, -0.6753616220517687507 ) ) ;
#14984=EDGE_CURVE ( 'NONE', #11891, #6348, #30705, .T. ) ;
#14988=EDGE_LOOP ( 'NONE', ( #31762, #6726, #20042, #13400, #8682, #19538, #38207, #5480, #17881, #20801, #11075, #12954 ) ) ;
#14989=ORIENTED_EDGE ( 'NONE', *, *, #25537, .F. ) ;
#15001=DIRECTION ( 'NONE',  ( -1.000000000000000000, -0.000000000000000000, -0.000000000000000000 ) ) ;
#15011=ADVANCED_FACE ( 'NONE', ( #2926 ), #15480, .F. ) ;
#15015=ORIENTED_EDGE ( 'NONE', *, *, #31218, .F. ) ;
#15022=DIRECTION ( 'NONE',  ( 1.000000000000000000, 0.000000000000000000, 0.000000000000000000 ) ) ;
#15027=ORIENTED_EDGE ( 'NONE', *, *, #33305, .T. ) ;
#15036=ORIENTED_EDGE ( 'NONE', *, *, #18557, .T. ) ;
#15049=CARTESIAN_POINT ( 'NONE',  ( -0.3000000000000000999, -3.705001275441084818, -0.3950781284944321903 ) ) ;
#15055=CARTESIAN_POINT ( 'NONE',  ( -0.3000000000000000999, -2.292669950144801572, -0.8383185228372386222 ) ) ;
#15072=EDGE_LOOP ( 'NONE', ( #22841, #1983, #28431, #32910 ) ) ;
#15089=FACE_OUTER_BOUND ( 'NONE', #18157, .T. ) ;
#15103=ORIENTED_EDGE ( 'NONE', *, *, #17031, .F. ) ;
#15113=CARTESIAN_POINT ( 'NONE',  ( -0.2746410161513779258, -2.595429044015121534, -0.5484989581857646623 ) ) ;
#15170=LINE ( 'NONE', #33914, #27008 ) ;
#15173=ORIENTED_EDGE ( 'NONE', *, *, #27502, .T. ) ;
#15180=ORIENTED_EDGE ( 'NONE', *, *, #11510, .F. ) ;
#15192=ADVANCED_FACE ( 'NONE', ( #36358 ), #25053, .F. ) ;
#15203=CIRCLE ( 'NONE', #7278, 0.1946589359789743512 ) ;
#15205=VECTOR ( 'NONE', #1047, 39.37007874015748143 ) ;
#15207=DIRECTION ( 'NONE',  ( 0.000000000000000000, -0.7071067811865475727, 0.7071067811865475727 ) ) ;
#15211=ORIENTED_EDGE ( 'NONE', *, *, #10636, .T. ) ;
#15218=ORIENTED_EDGE ( 'NONE', *, *, #7672, .T. ) ;
#15230=DIRECTION ( 'NONE',  ( 0.4999999999999963918, 0.3085698060533155762, 0.8091876635195464074 ) ) ;
#15239=CIRCLE ( 'NONE', #6028, 0.03999999999999933470 ) ;
#15240=CARTESIAN_POINT ( 'NONE',  ( -0.3000000000000000999, -4.162452804151155483, -0.5855328176471856771 ) ) ;
#15256=EDGE_CURVE ( 'NONE', #20453, #29444, #36759, .T. ) ;
#15278=CARTESIAN_POINT ( 'NONE',  ( -0.2399999999999999079, -3.941790907013290823, -0.009415996779116623042 ) ) ;
#15302=CARTESIAN_POINT ( 'NONE',  ( -0.2746410161513779258, -2.154189217240303655, -0.3012881438978376458 ) ) ;
#15354=AXIS2_PLACEMENT_3D ( 'NONE', #4765, #7239, #23538 ) ;
#15363=DIRECTION ( 'NONE',  ( 0.000000000000000000, 0.000000000000000000, -1.000000000000000000 ) ) ;
#15364=AXIS2_PLACEMENT_3D ( 'NONE', #2093, #40547, #18136 ) ;
#15365=EDGE_LOOP ( 'NONE', ( #26304, #38350, #32360, #12475 ) ) ;
#15386=EDGE_LOOP ( 'NONE', ( #35166, #29394, #34305, #28428 ) ) ;
#15397=CIRCLE ( 'NONE', #20664, 0.1000000000000000194 ) ;
#15414=DIRECTION ( 'NONE',  ( -1.000000000000000000, -0.000000000000000000, -0.000000000000000000 ) ) ;
#15415=CIRCLE ( 'NONE', #6215, 0.1600000000000006972 ) ;
#15416=AXIS2_PLACEMENT_3D ( 'NONE', #851, #38457, #28797 ) ;
#15420=DIRECTION ( 'NONE',  ( 0.000000000000000000, 0.000000000000000000, -1.000000000000000000 ) ) ;
#15422=EDGE_CURVE ( 'NONE', #33790, #2621, #38165, .T. ) ;
#15425=ORIENTED_EDGE ( 'NONE', *, *, #25229, .T. ) ;
#15464=CARTESIAN_POINT ( 'NONE',  ( -0.3000000000000000999, -3.525450504378606187, -0.1357627943591874498 ) ) ;
#15480=CYLINDRICAL_SURFACE ( 'NONE', #34877, 0.1000000000000000194 ) ;
#15496=LINE ( 'NONE', #28231, #157 ) ;
#15497=ORIENTED_EDGE ( 'NONE', *, *, #14224, .T. ) ;
#15505=VERTEX_POINT ( 'NONE', #39592 ) ;
#15514=CARTESIAN_POINT ( 'NONE',  ( -0.2746410161513782033, -2.376910030844113564, -0.7058185084100425666 ) ) ;
#15530=AXIS2_PLACEMENT_3D ( 'NONE', #38244, #34565, #16446 ) ;
#15535=CARTESIAN_POINT ( 'NONE',  ( -0.2746410161513779258, -2.068584980338025847, -0.2731141320652226145 ) ) ;
#15545=AXIS2_PLACEMENT_3D ( 'NONE', #19619, #726, #25797 ) ;
#15547=ORIENTED_EDGE ( 'NONE', *, *, #29125, .T. ) ;
#15551=DIRECTION ( 'NONE',  ( -1.000000000000000000, 0.000000000000000000, 0.000000000000000000 ) ) ;
#15555=DIRECTION ( 'NONE',  ( -1.000000000000000000, -0.000000000000000000, -0.000000000000000000 ) ) ;
#15575=CARTESIAN_POINT ( 'NONE',  ( -0.2746410161513782033, -2.461298705151934829, -0.7594706439553173816 ) ) ;
#15597=ORIENTED_EDGE ( 'NONE', *, *, #19748, .F. ) ;
#15600=LINE ( 'NONE', #2447, #39725 ) ;
#15603=ORIENTED_EDGE ( 'NONE', *, *, #35075, .F. ) ;
#15631=ORIENTED_EDGE ( 'NONE', *, *, #31371, .T. ) ;
#15654=CIRCLE ( 'NONE', #38635, 0.1600000000000006417 ) ;
#15694=EDGE_CURVE ( 'NONE', #36543, #28382, #6260, .T. ) ;
#15710=EDGE_CURVE ( 'NONE', #26723, #19496, #2116, .T. ) ;
#15714=CARTESIAN_POINT ( 'NONE',  ( -0.3000000000000000999, -3.985676108854518507, -0.6623095129438225648 ) ) ;
#15737=UNCERTAINTY_MEASURE_WITH_UNIT (LENGTH_MEASURE( 1.000000000000000082E-05 ), #1126, 'distance_accuracy_value', 'NONE');
#15748=EDGE_CURVE ( 'NONE', #9066, #1786, #18530, .T. ) ;
#15775=DIRECTION ( 'NONE',  ( 0.8660254037844385966, 0.4219433715391051054, 0.2682606777263730202 ) ) ;
#15778=ORIENTED_EDGE ( 'NONE', *, *, #30348, .T. ) ;
#15790=EDGE_LOOP ( 'NONE', ( #1347, #9796, #5835, #28845, #24627 ) ) ;
#15797=DIRECTION ( 'NONE',  ( 1.000000000000000000, 0.000000000000000000, 0.000000000000000000 ) ) ;
#15798=AXIS2_PLACEMENT_3D ( 'NONE', #35602, #19981, #4336 ) ;
#15800=VERTEX_POINT ( 'NONE', #19632 ) ;
#15803=FACE_OUTER_BOUND ( 'NONE', #2451, .T. ) ;
#15813=CARTESIAN_POINT ( 'NONE',  ( -0.3000000000000000999, -1.835749455202394298, -0.2938319975228648739 ) ) ;
#15821=EDGE_CURVE ( 'NONE', #12108, #39819, #13246, .T. ) ;
#15824=CONICAL_SURFACE ( 'NONE', #17779, 0.1946589359789742957, 1.047197551196600962 ) ;
#15844=ORIENTED_EDGE ( 'NONE', *, *, #35685, .T. ) ;
#15851=ADVANCED_FACE ( 'NONE', ( #19438 ), #4067, .F. ) ;
#15853=CIRCLE ( 'NONE', #21118, 0.1000000000000000194 ) ;
#15856=CIRCLE ( 'NONE', #20466, 0.1600000000000016964 ) ;
#15882=VERTEX_POINT ( 'NONE', #35450 ) ;
#15886=VECTOR ( 'NONE', #7192, 39.37007874015748854 ) ;
#15887=DIRECTION ( 'NONE',  ( 1.000000000000000000, -0.000000000000000000, -0.000000000000000000 ) ) ;
#15903=CARTESIAN_POINT ( 'NONE',  ( -0.2746410161513776482, -3.849534981189179028, -0.2910928155360645864 ) ) ;
#15905=CARTESIAN_POINT ( 'NONE',  ( -0.3000000000000000999, -2.599675038826658735, -0.8213992999509311943 ) ) ;
#15907=DIRECTION ( 'NONE',  ( -0.4999999999999988898, -0.6123724356957954695, 0.6123724356957944703 ) ) ;
#15927=VERTEX_POINT ( 'NONE', #1148 ) ;
#15930=CARTESIAN_POINT ( 'NONE',  ( -0.2399999999999999079, -4.394818335734379744, -0.8816972205720928768 ) ) ;
#15931=CARTESIAN_POINT ( 'NONE',  ( -0.2746410161513770931, -2.599675038826658735, -0.8213992999509311943 ) ) ;
#15933=EDGE_LOOP ( 'NONE', ( #21993, #28154, #28687, #9087 ) ) ;
#15950=CARTESIAN_POINT ( 'NONE',  ( -0.2746410161513770931, -3.525450504378606187, -0.1357627943591874498 ) ) ;
#15966=DIRECTION ( 'NONE',  ( -0.000000000000000000, 0.9246857012436749956, -0.3807313408632033713 ) ) ;
#15968=DIRECTION ( 'NONE',  ( -0.000000000000000000, 0.8438867430782084345, 0.5365213554527479278 ) ) ;
#15971=VECTOR ( 'NONE', #12126, 39.37007874015748854 ) ;
#15973=ORIENTED_EDGE ( 'NONE', *, *, #37674, .F. ) ;
#15978=CARTESIAN_POINT ( 'NONE',  ( -0.2399999999999999079, -1.804235510932644004, -0.1501860188971498311 ) ) ;
#15985=CARTESIAN_POINT ( 'NONE',  ( -0.3000000000000000999, -2.809880844172510272, -0.2480969101616946337 ) ) ;
#16043=LINE ( 'NONE', #38038, #21087 ) ;
#16047=LINE ( 'NONE', #32257, #40340 ) ;
#16067=CARTESIAN_POINT ( 'NONE',  ( -0.2399999999999999079, -2.292669950144801572, -0.8383185228372386222 ) ) ;
#16072=EDGE_CURVE ( 'NONE', #17308, #9809, #31721, .T. ) ;
#16101=VECTOR ( 'NONE', #320, 39.37007874015748854 ) ;
#16102=ADVANCED_FACE ( 'NONE', ( #19394 ), #35413, .F. ) ;
#16103=ORIENTED_EDGE ( 'NONE', *, *, #36894, .F. ) ;
#16104=ORIENTED_EDGE ( 'NONE', *, *, #4913, .T. ) ;
#16129=EDGE_CURVE ( 'NONE', #12691, #6348, #19247, .T. ) ;
#16130=CARTESIAN_POINT ( 'NONE',  ( -0.2746410161513779258, -3.527715956914472706, -0.3920205355121876289 ) ) ;
#16150=DIRECTION ( 'NONE',  ( 0.000000000000000000, 0.000000000000000000, -1.000000000000000000 ) ) ;
#16161=ORIENTED_EDGE ( 'NONE', *, *, #15710, .T. ) ;
#16164=EDGE_LOOP ( 'NONE', ( #32722, #15103, #6154, #13046 ) ) ;
#16200=DIRECTION ( 'NONE',  ( 0.000000000000000000, 0.000000000000000000, -1.000000000000000000 ) ) ;
#16220=VERTEX_POINT ( 'NONE', #7632 ) ;
#16221=DIRECTION ( 'NONE',  ( -1.000000000000000000, -0.000000000000000000, -0.000000000000000000 ) ) ;
#16228=ADVANCED_FACE ( 'NONE', ( #30238 ), #17509, .T. ) ;
#16237=CARTESIAN_POINT ( 'NONE',  ( -0.2399999999999999079, -3.941790907013290823, -0.4709369376873030477 ) ) ;
#16240=DIRECTION ( 'NONE',  ( 0.000000000000000000, -0.5781348229923771731, 0.8159412518334715481 ) ) ;
#16243=CARTESIAN_POINT ( 'NONE',  ( -0.3000000000000000999, -3.730063144961804245, -0.1064410973704724289 ) ) ;
#16246=ORIENTED_EDGE ( 'NONE', *, *, #27283, .T. ) ;
#16262=DIRECTION ( 'NONE',  ( -0.4999999999999968359, 0.7308273574226419322, 0.4646411234949411884 ) ) ;
#16270=DIRECTION ( 'NONE',  ( 0.000000000000000000, -0.5365213554527457074, 0.8438867430782097667 ) ) ;
#16274=LINE ( 'NONE', #673, #31093 ) ;
#16277=CARTESIAN_POINT ( 'NONE',  ( -0.3000000000000000999, -2.416006048095809877, -1.059240699271965402 ) ) ;
#16291=EDGE_CURVE ( 'NONE', #26127, #9912, #27777, .T. ) ;
#16293=EDGE_LOOP ( 'NONE', ( #32088, #28831, #30049, #17688 ) ) ;
#16334=LINE ( 'NONE', #19624, #16772 ) ;
#16348=FACE_OUTER_BOUND ( 'NONE', #31811, .T. ) ;
#16363=DIRECTION ( 'NONE',  ( 0.000000000000000000, 0.5365213554527465956, -0.8438867430782092116 ) ) ;
#16373=ORIENTED_EDGE ( 'NONE', *, *, #4922, .T. ) ;
#16374=CARTESIAN_POINT ( 'NONE',  ( -0.3000000000000000999, -2.778907721888695281, -0.2599079779360263798 ) ) ;
#16389=DIRECTION ( 'NONE',  ( 1.000000000000000000, -0.000000000000000000, -0.000000000000000000 ) ) ;
#16398=ORIENTED_EDGE ( 'NONE', *, *, #2671, .T. ) ;
#16399=DIRECTION ( 'NONE',  ( -1.000000000000000000, -0.000000000000000000, -0.000000000000000000 ) ) ;
#16404=CARTESIAN_POINT ( 'NONE',  ( -0.3000000000000000999, -3.941790907013290823, -0.4709369376873030477 ) ) ;
#16417=CARTESIAN_POINT ( 'NONE',  ( -0.2399999999999999079, -3.880844374714816247, -0.2860650318788287017 ) ) ;
#16423=CARTESIAN_POINT ( 'NONE',  ( -0.2399999999999999079, -3.291368864184588183, -0.6988176298300771139 ) ) ;
#16434=CIRCLE ( 'NONE', #36803, 0.1600000000000001976 ) ;
#16446=DIRECTION ( 'NONE',  ( 0.000000000000000000, 0.000000000000000000, -1.000000000000000000 ) ) ;
#16473=AXIS2_PLACEMENT_3D ( 'NONE', #18506, #30662, #18310 ) ;
#16474=FACE_OUTER_BOUND ( 'NONE', #9556, .T. ) ;
#16479=ORIENTED_EDGE ( 'NONE', *, *, #13158, .F. ) ;
#16481=CARTESIAN_POINT ( 'NONE',  ( -0.3000000000000000999, -2.003129936916423048, -0.4197911229995844873 ) ) ;
#16507=CIRCLE ( 'NONE', #36876, 0.03999999999999964001 ) ;
#16523=VECTOR ( 'NONE', #21322, 39.37007874015748143 ) ;
#16524=DIRECTION ( 'NONE',  ( 0.4999999999999993894, 0.000000000000000000, -0.8660254037844390407 ) ) ;
#16527=CIRCLE ( 'NONE', #11913, 0.1000000000000000194 ) ;
#16547=FACE_OUTER_BOUND ( 'NONE', #8725, .T. ) ;
#16569=DIRECTION ( 'NONE',  ( 0.000000000000000000, 0.000000000000000000, -1.000000000000000000 ) ) ;
#16576=ORIENTED_EDGE ( 'NONE', *, *, #5674, .F. ) ;
#16577=DIRECTION ( 'NONE',  ( -0.000000000000000000, 0.3807313408632033713, 0.9246857012436752177 ) ) ;
#16600=DIRECTION ( 'NONE',  ( 0.000000000000000000, 0.000000000000000000, -1.000000000000000000 ) ) ;
#16618=CIRCLE ( 'NONE', #8059, 0.1000000000000000194 ) ;
#16626=DIRECTION ( 'NONE',  ( 1.000000000000000000, 0.000000000000000000, 0.000000000000000000 ) ) ;
#16629=AXIS2_PLACEMENT_3D ( 'NONE', #24312, #27595, #30880 ) ;
#16639=ORIENTED_EDGE ( 'NONE', *, *, #25219, .F. ) ;
#16645=ORIENTED_EDGE ( 'NONE', *, *, #29833, .T. ) ;
#16664=AXIS2_PLACEMENT_3D ( 'NONE', #19048, #9982, #25837 ) ;
#16669=DIRECTION ( 'NONE',  ( 1.000000000000000000, -0.000000000000000000, -0.000000000000000000 ) ) ;
#16694=EDGE_LOOP ( 'NONE', ( #37943, #26771, #27679, #40525 ) ) ;
#16710=VECTOR ( 'NONE', #35308, 39.37007874015748143 ) ;
#16721=FACE_OUTER_BOUND ( 'NONE', #16953, .T. ) ;
#16736=DIRECTION ( 'NONE',  ( 0.000000000000000000, -0.8438867430782093226, -0.5365213554527464845 ) ) ;
#16745=DIRECTION ( 'NONE',  ( 1.000000000000000000, 0.000000000000000000, 0.000000000000000000 ) ) ;
#16748=AXIS2_PLACEMENT_3D ( 'NONE', #7129, #19697, #16827 ) ;
#16759=CARTESIAN_POINT ( 'NONE',  ( -0.2399999999999999079, -3.811657270145150989, -0.1642545796697100491 ) ) ;
#16772=VECTOR ( 'NONE', #6849, 39.37007874015748143 ) ;
#16782=EDGE_CURVE ( 'NONE', #32375, #27977, #8582, .T. ) ;
#16789=EDGE_CURVE ( 'NONE', #18610, #27000, #28481, .T. ) ;
#16796=FACE_OUTER_BOUND ( 'NONE', #17612, .T. ) ;
#16800=ADVANCED_FACE ( 'NONE', ( #16547 ), #4124, .F. ) ;
#16827=DIRECTION ( 'NONE',  ( 0.000000000000000000, 0.9343694307158671997, -0.3563057211773426602 ) ) ;
#16858=CARTESIAN_POINT ( 'NONE',  ( -0.2399999999999999079, -3.745280840418592661, 0.04438736989695814261 ) ) ;
#16887=CARTESIAN_POINT ( 'NONE',  ( -0.3000000000000000999, -3.220869926774937664, -0.5656276768926112863 ) ) ;
#16901=ORIENTED_EDGE ( 'NONE', *, *, #2257, .F. ) ;
#16911=VERTEX_POINT ( 'NONE', #14456 ) ;
#16923=CARTESIAN_POINT ( 'NONE',  ( -0.3000000000000000999, -3.723902497147952406, 0.1004495357399106253 ) ) ;
#16928=FACE_OUTER_BOUND ( 'NONE', #8428, .T. ) ;
#16936=PLANE ( 'NONE',  #15354 ) ;
#16953=EDGE_LOOP ( 'NONE', ( #25302, #15015, #4257, #5242 ) ) ;
#16965=EDGE_CURVE ( 'NONE', #36975, #20955, #27025, .T. ) ;
#16966=CARTESIAN_POINT ( 'NONE',  ( -0.2746410161513770931, -2.909786385774835171, -0.3705357231075770419 ) ) ;
#16973=DIRECTION ( 'NONE',  ( -1.000000000000000000, 0.000000000000000000, 0.000000000000000000 ) ) ;
#16984=ORIENTED_EDGE ( 'NONE', *, *, #26367, .T. ) ;
#17000=ORIENTED_EDGE ( 'NONE', *, *, #21836, .T. ) ;
#17012=LINE ( 'NONE', #1395, #27392 ) ;
#17026=ADVANCED_FACE ( 'NONE', ( #16474 ), #21895, .F. ) ;
#17031=EDGE_CURVE ( 'NONE', #17308, #25560, #880, .T. ) ;
#17039=CARTESIAN_POINT ( 'NONE',  ( -0.2399999999999999079, -4.233163482269810096, -0.5148221395285308422 ) ) ;
#17040=CARTESIAN_POINT ( 'NONE',  ( -0.2746410161513782033, -2.253314830856113726, -0.6753616220517687507 ) ) ;
#17051=CARTESIAN_POINT ( 'NONE',  ( -0.2399999999999999079, -2.511040369707300268, -0.6548468226404909887 ) ) ;
#17052=EDGE_LOOP ( 'NONE', ( #23231, #40318, #18218, #35266 ) ) ;
#17067=DIRECTION ( 'NONE',  ( 0.000000000000000000, -0.5781348229923759519, 0.8159412518334724362 ) ) ;
#17073=EDGE_CURVE ( 'NONE', #15505, #22378, #10917, .T. ) ;
#17074=EDGE_CURVE ( 'NONE', #9066, #7581, #29432, .T. ) ;
#17079=LINE ( 'NONE', #11527, #25203 ) ;
#17093=ORIENTED_EDGE ( 'NONE', *, *, #29097, .T. ) ;
#17095=CARTESIAN_POINT ( 'NONE',  ( -0.2399999999999999079, -3.941790907013290823, -0.4709369376873030477 ) ) ;
#17099=DIRECTION ( 'NONE',  ( 0.000000000000000000, 0.5365213554527455964, -0.8438867430782097667 ) ) ;
#17104=ORIENTED_EDGE ( 'NONE', *, *, #17915, .T. ) ;
#17163=VECTOR ( 'NONE', #4626, 39.37007874015748143 ) ;
#17178=CARTESIAN_POINT ( 'NONE',  ( -0.2746410161513782033, -1.962518963160043706, -0.3791801492432048115 ) ) ;
#17188=ORIENTED_EDGE ( 'NONE', *, *, #5740, .F. ) ;
#17205=EDGE_CURVE ( 'NONE', #6967, #33790, #9295, .T. ) ;
#17241=ORIENTED_EDGE ( 'NONE', *, *, #5721, .F. ) ;
#17245=FACE_OUTER_BOUND ( 'NONE', #17690, .T. ) ;
#17255=EDGE_CURVE ( 'NONE', #2786, #27821, #3516, .T. ) ;
#17262=DIRECTION ( 'NONE',  ( -1.000000000000000000, 0.000000000000000000, 0.000000000000000000 ) ) ;
#17264=CARTESIAN_POINT ( 'NONE',  ( -0.3000000000000000999, -2.853330612949663170, -0.6088139570729240724 ) ) ;
#17272=DIRECTION ( 'NONE',  ( 1.000000000000000000, 0.000000000000000000, 0.000000000000000000 ) ) ;
#17282=DIRECTION ( 'NONE',  ( -1.000000000000000000, -0.000000000000000000, -0.000000000000000000 ) ) ;
#17286=DIRECTION ( 'NONE',  ( 1.000000000000000000, -0.000000000000000000, -0.000000000000000000 ) ) ;
#17291=EDGE_LOOP ( 'NONE', ( #12499, #20206, #10367, #6440 ) ) ;
#17306=EDGE_CURVE ( 'NONE', #22862, #21137, #37877, .T. ) ;
#17308=VERTEX_POINT ( 'NONE', #40341 ) ;
#17347=CYLINDRICAL_SURFACE ( 'NONE', #26516, 0.06250000000000001388 ) ;
#17356=CARTESIAN_POINT ( 'NONE',  ( -0.2399999999999999079, -3.216935334666387813, -0.6321346234654038332 ) ) ;
#17359=ORIENTED_EDGE ( 'NONE', *, *, #14316, .T. ) ;
#17373=DIRECTION ( 'NONE',  ( 1.000000000000000000, 0.000000000000000000, 0.000000000000000000 ) ) ;
#17375=CONICAL_SURFACE ( 'NONE', #25247, 0.1600000000000006417, 1.047197551196599408 ) ;
#17407=ORIENTED_EDGE ( 'NONE', *, *, #23002, .F. ) ;
#17428=EDGE_CURVE ( 'NONE', #22034, #20195, #32962, .T. ) ;
#17437=CARTESIAN_POINT ( 'NONE',  ( -0.2746410161513782033, -1.739646749720735741, -0.3661865639197241507 ) ) ;
#17439=EDGE_CURVE ( 'NONE', #9666, #18610, #29681, .T. ) ;
#17449=ORIENTED_EDGE ( 'NONE', *, *, #5936, .T. ) ;
#17451=CARTESIAN_POINT ( 'NONE',  ( -0.2746410161513782033, -2.183180860297908144, -0.4937760292030871079 ) ) ;
#17460=DIRECTION ( 'NONE',  ( 0.4999999999999988343, 0.000000000000000000, -0.8660254037844393737 ) ) ;
#17467=DIRECTION ( 'NONE',  ( -0.3779644730092284188, 0.9258200997725509751, 0.000000000000000000 ) ) ;
#17481=AXIS2_PLACEMENT_3D ( 'NONE', #2212, #8557, #29567 ) ;
#17496=VECTOR ( 'NONE', #27540, 39.37007874015748143 ) ;
#17501=VERTEX_POINT ( 'NONE', #38480 ) ;
#17509=CYLINDRICAL_SURFACE ( 'NONE', #25798, 0.1946589359789743512 ) ;
#17527=DIRECTION ( 'NONE',  ( 0.000000000000000000, 0.9246857012436752177, -0.3807313408632029827 ) ) ;
#17538=AXIS2_PLACEMENT_3D ( 'NONE', #9468, #30872, #267 ) ;
#17546=EDGE_CURVE ( 'NONE', #34948, #36123, #10910, .T. ) ;
#17549=LINE ( 'NONE', #9494, #28507 ) ;
#17554=DIRECTION ( 'NONE',  ( 0.000000000000000000, -0.9343694307158671997, 0.3563057211773426602 ) ) ;
#17560=VERTEX_POINT ( 'NONE', #11902 ) ;
#17567=VERTEX_POINT ( 'NONE', #18089 ) ;
#17576=ORIENTED_EDGE ( 'NONE', *, *, #26983, .F. ) ;
#17587=DIRECTION ( 'NONE',  ( 0.000000000000000000, 0.000000000000000000, -1.000000000000000000 ) ) ;
#17612=EDGE_LOOP ( 'NONE', ( #34516, #36426, #3032, #5028 ) ) ;
#17623=EDGE_LOOP ( 'NONE', ( #11480, #35226, #29099, #10784 ) ) ;
#17628=DIRECTION ( 'NONE',  ( -1.000000000000000000, 0.000000000000000000, 0.000000000000000000 ) ) ;
#17646=DIRECTION ( 'NONE',  ( 0.000000000000000000, -0.8159412518334726583, -0.5781348229923756188 ) ) ;
#17676=CARTESIAN_POINT ( 'NONE',  ( -0.2399999999999999079, -3.941790907013290823, 0.1405840032208834911 ) ) ;
#17687=CARTESIAN_POINT ( 'NONE',  ( -0.2746410161513779258, -2.511040369707300268, -0.4948468226404901804 ) ) ;
#17688=ORIENTED_EDGE ( 'NONE', *, *, #3900, .F. ) ;
#17690=EDGE_LOOP ( 'NONE', ( #17884, #10626, #36422, #25573 ) ) ;
#17713=FACE_OUTER_BOUND ( 'NONE', #26125, .T. ) ;
#17749=CARTESIAN_POINT ( 'NONE',  ( -0.2399999999999999079, -2.375007723916885194, -0.5268601001523036675 ) ) ;
#17755=VECTOR ( 'NONE', #29071, 39.37007874015748143 ) ;
#17759=EDGE_CURVE ( 'NONE', #2621, #22034, #24685, .T. ) ;
#17779=AXIS2_PLACEMENT_3D ( 'NONE', #8789, #2625, #6310 ) ;
#17799=ORIENTED_EDGE ( 'NONE', *, *, #29129, .F. ) ;
#17805=EDGE_CURVE ( 'NONE', #12532, #34047, #19207, .T. ) ;
#17806=ORIENTED_EDGE ( 'NONE', *, *, #13417, .T. ) ;
#17807=CIRCLE ( 'NONE', #117, 0.1000000000000000194 ) ;
#17810=AXIS2_PLACEMENT_3D ( 'NONE', #39671, #21588, #40495 ) ;
#17819=CARTESIAN_POINT ( 'NONE',  ( -0.2746410161513779258, -3.941790907013290823, -0.4709369376873030477 ) ) ;
#17856=ORIENTED_EDGE ( 'NONE', *, *, #30348, .F. ) ;
#17878=LINE ( 'NONE', #30445, #24570 ) ;
#17879=DIRECTION ( 'NONE',  ( 0.000000000000000000, 0.000000000000000000, -1.000000000000000000 ) ) ;
#17881=ORIENTED_EDGE ( 'NONE', *, *, #23575, .T. ) ;
#17884=ORIENTED_EDGE ( 'NONE', *, *, #39553, .T. ) ;
#17896=DIRECTION ( 'NONE',  ( 0.000000000000000000, 0.000000000000000000, -1.000000000000000000 ) ) ;
#17911=DIRECTION ( 'NONE',  ( 0.000000000000000000, 0.8159412518334721032, 0.5781348229923763959 ) ) ;
#17915=EDGE_CURVE ( 'NONE', #7075, #34890, #36903, .T. ) ;
#17925=EDGE_CURVE ( 'NONE', #40377, #14064, #15239, .T. ) ;
#17961=CARTESIAN_POINT ( 'NONE',  ( -0.2399999999999999079, -3.985676108854518507, -0.7623095129438225426 ) ) ;
#17965=ORIENTED_EDGE ( 'NONE', *, *, #22888, .T. ) ;
#17969=VECTOR ( 'NONE', #15966, 39.37007874015748854 ) ;
#17971=ADVANCED_FACE ( 'NONE', ( #14082 ), #39191, .T. ) ;
#17974=DIRECTION ( 'NONE',  ( 0.4747798520620616913, 0.000000000000000000, -0.8801045915548485477 ) ) ;
#17984=DIRECTION ( 'NONE',  ( 1.000000000000000000, 0.000000000000000000, 0.000000000000000000 ) ) ;
#17987=CIRCLE ( 'NONE', #23276, 0.1000000000000000194 ) ;
#17989=ORIENTED_EDGE ( 'NONE', *, *, #35078, .F. ) ;
#17993=VECTOR ( 'NONE', #28496, 39.37007874015748854 ) ;
#17997=VECTOR ( 'NONE', #20785, 39.37007874015748854 ) ;
#18007=ORIENTED_EDGE ( 'NONE', *, *, #31371, .F. ) ;
#18022=VECTOR ( 'NONE', #16745, 39.37007874015748143 ) ;
#18024=CIRCLE ( 'NONE', #336, 0.1000000000000000194 ) ;
#18025=DIRECTION ( 'NONE',  ( 0.000000000000000000, -0.7071067811865474617, -0.7071067811865474617 ) ) ;
#18039=CYLINDRICAL_SURFACE ( 'NONE', #11601, 0.1000000000000000194 ) ;
#18045=CARTESIAN_POINT ( 'NONE',  ( -0.2746410161513782033, -1.835749455202394298, -0.3938319975228649072 ) ) ;
#18050=EDGE_CURVE ( 'NONE', #24506, #27821, #31356, .T. ) ;
#18051=CIRCLE ( 'NONE', #26617, 0.1000000000000000194 ) ;
#18066=EDGE_LOOP ( 'NONE', ( #3381, #27520, #36594, #3326 ) ) ;
#18077=ORIENTED_EDGE ( 'NONE', *, *, #5471, .F. ) ;
#18089=CARTESIAN_POINT ( 'NONE',  ( -0.2746410161513779258, -4.250025578259899461, -0.8852376261118949374 ) ) ;
#18090=DIRECTION ( 'NONE',  ( 0.000000000000000000, 0.000000000000000000, -1.000000000000000000 ) ) ;
#18132=LINE ( 'NONE', #36232, #20692 ) ;
#18136=DIRECTION ( 'NONE',  ( 0.3779644730092246441, 0.000000000000000000, 0.9258200997725524184 ) ) ;
#18157=EDGE_LOOP ( 'NONE', ( #7266, #38703, #26912, #20196 ) ) ;
#18213=EDGE_CURVE ( 'NONE', #25941, #26629, #26342, .T. ) ;
#18218=ORIENTED_EDGE ( 'NONE', *, *, #39336, .F. ) ;
#18238=LINE ( 'NONE', #28112, #36498 ) ;
#18245=LINE ( 'NONE', #27707, #35901 ) ;
#18247=ADVANCED_FACE ( 'NONE', ( #29834 ), #1466, .F. ) ;
#18250=DIRECTION ( 'NONE',  ( 0.000000000000000000, 0.000000000000000000, -1.000000000000000000 ) ) ;
#18262=EDGE_CURVE ( 'NONE', #31712, #9001, #23830, .T. ) ;
#18265=ORIENTED_EDGE ( 'NONE', *, *, #37528, .F. ) ;
#18267=ORIENTED_EDGE ( 'NONE', *, *, #21493, .F. ) ;
#18293=LINE ( 'NONE', #27962, #17997 ) ;
#18310=DIRECTION ( 'NONE',  ( 0.000000000000000000, 0.000000000000000000, 1.000000000000000000 ) ) ;
#18324=ORIENTED_EDGE ( 'NONE', *, *, #32560, .F. ) ;
#18341=DIRECTION ( 'NONE',  ( 0.000000000000000000, 0.000000000000000000, -1.000000000000000000 ) ) ;
#18391=LINE ( 'NONE', #28081, #4213 ) ;
#18395=ORIENTED_EDGE ( 'NONE', *, *, #26543, .T. ) ;
#18403=CARTESIAN_POINT ( 'NONE',  ( -0.2399999999999999079, -3.194091454214595949, -0.5766534813907827628 ) ) ;
#18421=CARTESIAN_POINT ( 'NONE',  ( -0.2399999999999999079, -3.899630010830198668, -0.3430483616844877681 ) ) ;
#18425=CARTESIAN_POINT ( 'NONE',  ( -0.2746410161513782033, -2.322955634169589612, -0.9336221289765171960 ) ) ;
#18456=VERTEX_POINT ( 'NONE', #15813 ) ;
#18460=CARTESIAN_POINT ( 'NONE',  ( -0.2399999999999999079, -2.888408042504194473, -0.3144735572646252253 ) ) ;
#18461=ORIENTED_EDGE ( 'NONE', *, *, #23796, .F. ) ;
#18467=DIRECTION ( 'NONE',  ( 0.000000000000000000, 0.000000000000000000, -1.000000000000000000 ) ) ;
#18474=PLANE ( 'NONE',  #4876 ) ;
#18488=AXIS2_PLACEMENT_3D ( 'NONE', #6001, #9097, #7358 ) ;
#18494=CIRCLE ( 'NONE', #27047, 0.1946589359789743512 ) ;
#18501=EDGE_LOOP ( 'NONE', ( #32614, #9308, #7400, #30397 ) ) ;
#18506=CARTESIAN_POINT ( 'NONE',  ( -0.2399999999999999079, -2.183180860297908144, -0.4937760292030871079 ) ) ;
#18507=DIRECTION ( 'NONE',  ( -0.4999999999999977240, 0.4646411234949380242, -0.7308273574226432645 ) ) ;
#18511=ORIENTED_EDGE ( 'NONE', *, *, #20793, .T. ) ;
#18530=CIRCLE ( 'NONE', #29040, 0.06250000000000001388 ) ;
#18533=ADVANCED_FACE ( 'NONE', ( #13728 ), #23223, .T. ) ;
#18538=ADVANCED_FACE ( 'NONE', ( #3866 ), #1229, .F. ) ;
#18546=AXIS2_PLACEMENT_3D ( 'NONE', #4696, #20569, #26935 ) ;
#18548=CARTESIAN_POINT ( 'NONE',  ( -0.2399999999999999079, -4.233163482269810096, -0.5148221395285308422 ) ) ;
#18557=EDGE_CURVE ( 'NONE', #15927, #6967, #25909, .T. ) ;
#18572=VERTEX_POINT ( 'NONE', #36751 ) ;
#18586=AXIS2_PLACEMENT_3D ( 'NONE', #1568, #8111, #12377 ) ;
#18598=AXIS2_PLACEMENT_3D ( 'NONE', #4549, #14022, #1716 ) ;
#18606=DIRECTION ( 'NONE',  ( 1.000000000000000000, -0.000000000000000000, -0.000000000000000000 ) ) ;
#18610=VERTEX_POINT ( 'NONE', #17437 ) ;
#18624=AXIS2_PLACEMENT_3D ( 'NONE', #21800, #15207, #21186 ) ;
#18632=UNCERTAINTY_MEASURE_WITH_UNIT (LENGTH_MEASURE( 1.000000000000000082E-05 ), #324, 'distance_accuracy_value', 'NONE');
#18652=DIRECTION ( 'NONE',  ( 0.000000000000000000, 0.000000000000000000, 1.000000000000000000 ) ) ;
#18654=ORIENTED_EDGE ( 'NONE', *, *, #6230, .T. ) ;
#18680=ORIENTED_EDGE ( 'NONE', *, *, #23002, .T. ) ;
#18681=EDGE_LOOP ( 'NONE', ( #34793, #22369, #6517, #2019 ) ) ;
#18689=DIRECTION ( 'NONE',  ( -0.000000000000000000, 0.7071067811865465735, 0.7071067811865484609 ) ) ;
#18694=ORIENTED_EDGE ( 'NONE', *, *, #7246, .T. ) ;
#18706=AXIS2_PLACEMENT_3D ( 'NONE', #40463, #8780, #18250 ) ;
#18707=AXIS2_PLACEMENT_3D ( 'NONE', #24111, #2291, #36635 ) ;
#18733=CIRCLE ( 'NONE', #1032, 0.4615209409081865166 ) ;
#18735=ADVANCED_FACE ( 'NONE', ( #39436 ), #39637, .T. ) ;
#18742=CYLINDRICAL_SURFACE ( 'NONE', #17538, 0.6115209409081865388 ) ;
#18748=FACE_OUTER_BOUND ( 'NONE', #13578, .T. ) ;
#18751=CONICAL_SURFACE ( 'NONE', #2308, 0.03999999999999933470, 1.047197551196598742 ) ;
#18752=CARTESIAN_POINT ( 'NONE',  ( -0.2746410161513776482, -4.162452804151155483, -0.5855328176471856771 ) ) ;
#18771=EDGE_LOOP ( 'NONE', ( #13830, #33867, #1251, #2369 ) ) ;
#18803=EDGE_CURVE ( 'NONE', #3165, #839, #16618, .T. ) ;
#18809=DIRECTION ( 'NONE',  ( 1.000000000000000000, -0.000000000000000000, -0.000000000000000000 ) ) ;
#18816=ADVANCED_FACE ( 'NONE', ( #9378 ), #9593, .T. ) ;
#18875=DIRECTION ( 'NONE',  ( 0.000000000000000000, 0.5365213554527478168, -0.8438867430782083234 ) ) ;
#18901=DIRECTION ( 'NONE',  ( 1.000000000000000000, -0.000000000000000000, -0.000000000000000000 ) ) ;
#18906=FACE_BOUND ( 'NONE', #33572, .T. ) ;
#18909=DIRECTION ( 'NONE',  ( 0.000000000000000000, 0.000000000000000000, 1.000000000000000000 ) ) ;
#18920=DIRECTION ( 'NONE',  ( 1.000000000000000000, 0.000000000000000000, 0.000000000000000000 ) ) ;
#18926=CONICAL_SURFACE ( 'NONE', #11022, 0.03999999999999964001, 1.047197551196596299 ) ;
#18929=DIRECTION ( 'NONE',  ( 0.4999999999999956701, 0.7066258520834639567, 0.5006794435238205443 ) ) ;
#18930=ORIENTED_EDGE ( 'NONE', *, *, #25580, .F. ) ;
#18952=CARTESIAN_POINT ( 'NONE',  ( -0.2399999999999999079, -3.849534981189179028, -0.1910928155360645808 ) ) ;
#18969=ORIENTED_EDGE ( 'NONE', *, *, #5663, .T. ) ;
#18996=LINE ( 'NONE', #31528, #27290 ) ;
#19000=LENGTH_MEASURE_WITH_UNIT ( LENGTH_MEASURE( 0.02539999999999999897 ), #3561 );
#19010=CARTESIAN_POINT ( 'NONE',  ( -0.2746410161513776482, -3.812085038045152974, -0.02801711824816590160 ) ) ;
#19017=ORIENTED_EDGE ( 'NONE', *, *, #15422, .T. ) ;
#19025=ADVANCED_FACE ( 'NONE', ( #29945 ), #26858, .T. ) ;
#19027=DIRECTION ( 'NONE',  ( 1.000000000000000000, 0.000000000000000000, 0.000000000000000000 ) ) ;
#19043=FACE_OUTER_BOUND ( 'NONE', #16164, .T. ) ;
#19048=CARTESIAN_POINT ( 'NONE',  ( -0.2399999999999999079, -2.853330612949663170, -0.6088139570729240724 ) ) ;
#19052=ADVANCED_FACE ( 'NONE', ( #2165 ), #39200, .T. ) ;
#19071=DIRECTION ( 'NONE',  ( -1.000000000000000000, -0.000000000000000000, -0.000000000000000000 ) ) ;
#19089=ORIENTED_EDGE ( 'NONE', *, *, #8172, .T. ) ;
#19090=AXIS2_PLACEMENT_3D ( 'NONE', #34085, #36970, #40472 ) ;
#19111=EDGE_CURVE ( 'NONE', #38965, #26127, #8326, .T. ) ;
#19124=VECTOR ( 'NONE', #25701, 39.37007874015748854 ) ;
#19150=CARTESIAN_POINT ( 'NONE',  ( -0.2399999999999999079, -2.811755946567116471, -0.3200729990151717774 ) ) ;
#19169=DIRECTION ( 'NONE',  ( 0.000000000000000000, -0.7071067811865474617, -0.7071067811865474617 ) ) ;
#19197=VERTEX_POINT ( 'NONE', #5983 ) ;
#19207=CIRCLE ( 'NONE', #20501, 0.1000000000000000194 ) ;
#19247=CIRCLE ( 'NONE', #25832, 0.1346589359789736318 ) ;
#19248=EDGE_CURVE ( 'NONE', #39819, #34187, #37460, .T. ) ;
#19249=FACE_OUTER_BOUND ( 'NONE', #21319, .T. ) ;
#19264=CARTESIAN_POINT ( 'NONE',  ( -0.2399999999999999079, -4.233163482269810096, -0.5148221395285308422 ) ) ;
#19266=CYLINDRICAL_SURFACE ( 'NONE', #9422, 0.1000000000000000194 ) ;
#19284=PLANE ( 'NONE',  #23948 ) ;
#19302=CARTESIAN_POINT ( 'NONE',  ( -0.3000000000000000999, -2.183180860297908144, -0.4937760292030871079 ) ) ;
#19305=VECTOR ( 'NONE', #1421, 39.37007874015748143 ) ;
#19334=CIRCLE ( 'NONE', #33087, 0.1600000000000005029 ) ;
#19381=DIRECTION ( 'NONE',  ( -1.000000000000000000, -0.000000000000000000, -0.000000000000000000 ) ) ;
#19386=DIRECTION ( 'NONE',  ( -0.4999999999999969469, 0.2622817173645498601, 0.8253534398888184853 ) ) ;
#19387=VECTOR ( 'NONE', #6057, 39.37007874015748143 ) ;
#19393=ORIENTED_EDGE ( 'NONE', *, *, #14984, .T. ) ;
#19394=FACE_OUTER_BOUND ( 'NONE', #12703, .T. ) ;
#19396=ORIENTED_EDGE ( 'NONE', *, *, #4372, .F. ) ;
#19416=AXIS2_PLACEMENT_3D ( 'NONE', #17264, #4905, #32695 ) ;
#19427=AXIS2_PLACEMENT_3D ( 'NONE', #9078, #34772, #6188 ) ;
#19429=VERTEX_POINT ( 'NONE', #2058 ) ;
#19438=FACE_OUTER_BOUND ( 'NONE', #14455, .T. ) ;
#19473=ADVANCED_FACE ( 'NONE', ( #5933 ), #34129, .F. ) ;
#19482=ADVANCED_FACE ( 'NONE', ( #23882 ), #22566, .F. ) ;
#19491=DIRECTION ( 'NONE',  ( 0.000000000000000000, -0.5365213554527469286, 0.8438867430782091006 ) ) ;
#19496=VERTEX_POINT ( 'NONE', #30446 ) ;
#19504=ORIENTED_EDGE ( 'NONE', *, *, #21203, .T. ) ;
#19516=CONICAL_SURFACE ( 'NONE', #1789, 0.1600000000000006972, 1.047197551196598297 ) ;
#19526=CARTESIAN_POINT ( 'NONE',  ( -0.2399999999999999079, -2.323257895298838971, -0.7902071827178637209 ) ) ;
#19535=ADVANCED_FACE ( 'NONE', ( #28173 ), #37839, .F. ) ;
#19538=ORIENTED_EDGE ( 'NONE', *, *, #12547, .T. ) ;
#19556=EDGE_CURVE ( 'NONE', #34622, #2786, #6750, .T. ) ;
#19573=DIRECTION ( 'NONE',  ( 0.000000000000000000, 0.000000000000000000, -1.000000000000000000 ) ) ;
#19587=VERTEX_POINT ( 'NONE', #9440 ) ;
#19589=VERTEX_POINT ( 'NONE', #16243 ) ;
#19610=CARTESIAN_POINT ( 'NONE',  ( -0.2399999999999999079, -4.350369088120884520, -0.8413950570247814564 ) ) ;
#19619=CARTESIAN_POINT ( 'NONE',  ( -0.3000000000000000999, -1.804235510932644004, -0.1501860188971498311 ) ) ;
#19624=CARTESIAN_POINT ( 'NONE',  ( -0.3000000000000000999, -3.217981293616048344, -0.2530108926800491709 ) ) ;
#19632=CARTESIAN_POINT ( 'NONE',  ( -0.2746410161513770931, -2.861028283584748699, -0.4103205306338890690 ) ) ;
#19637=DIRECTION ( 'NONE',  ( -1.000000000000000000, -0.000000000000000000, -0.000000000000000000 ) ) ;
#19638=VERTEX_POINT ( 'NONE', #23444 ) ;
#19655=DIRECTION ( 'NONE',  ( 1.000000000000000000, 0.000000000000000000, 0.000000000000000000 ) ) ;
#19679=LINE ( 'NONE', #32214, #40147 ) ;
#19697=DIRECTION ( 'NONE',  ( 0.000000000000000000, -0.3563057211773426602, -0.9343694307158671997 ) ) ;
#19724=CIRCLE ( 'NONE', #2003, 0.1600000000000000588 ) ;
#19743=FACE_OUTER_BOUND ( 'NONE', #21302, .T. ) ;
#19746=ADVANCED_FACE ( 'NONE', ( #35753 ), #31767, .F. ) ;
#19748=EDGE_CURVE ( 'NONE', #14090, #14891, #23631, .T. ) ;
#19761=CONICAL_SURFACE ( 'NONE', #6614, 0.5515209409081860414, 1.047197551196597409 ) ;
#19773=DIRECTION ( 'NONE',  ( 0.000000000000000000, 0.000000000000000000, -1.000000000000000000 ) ) ;
#19780=DIRECTION ( 'NONE',  ( 1.000000000000000000, -0.000000000000000000, -0.000000000000000000 ) ) ;
#19787=ORIENTED_EDGE ( 'NONE', *, *, #33417, .T. ) ;
#19792=AXIS2_PLACEMENT_3D ( 'NONE', #23100, #38909, #4744 ) ;
#19802=AXIS2_PLACEMENT_3D ( 'NONE', #13901, #26474, #29147 ) ;
#19807=EDGE_CURVE ( 'NONE', #38965, #19638, #2427, .T. ) ;
#19811=CYLINDRICAL_SURFACE ( 'NONE', #1781, 0.06250000000000001388 ) ;
#19825=EDGE_LOOP ( 'NONE', ( #40200, #7099, #3832, #20425 ) ) ;
#19848=EDGE_CURVE ( 'NONE', #27128, #7581, #6124, .T. ) ;
#19875=AXIS2_PLACEMENT_3D ( 'NONE', #38820, #13335, #10447 ) ;
#19877=FACE_OUTER_BOUND ( 'NONE', #9725, .T. ) ;
#19887=ORIENTED_EDGE ( 'NONE', *, *, #17205, .F. ) ;
#19907=VECTOR ( 'NONE', #33005, 39.37007874015748854 ) ;
#19928=DIRECTION ( 'NONE',  ( 0.000000000000000000, -3.414809992080312950E-15, -1.000000000000000000 ) ) ;
#19933=ORIENTED_EDGE ( 'NONE', *, *, #12042, .T. ) ;
#19938=AXIS2_PLACEMENT_3D ( 'NONE', #14958, #21740, #18652 ) ;
#19959=DIRECTION ( 'NONE',  ( 0.000000000000000000, 0.000000000000000000, -1.000000000000000000 ) ) ;
#19969=CARTESIAN_POINT ( 'NONE',  ( -0.2399999999999999079, -3.755970012053913010, 0.01635628697548255697 ) ) ;
#19972=DIRECTION ( 'NONE',  ( -1.000000000000000000, 0.000000000000000000, 0.000000000000000000 ) ) ;
#19974=CONICAL_SURFACE ( 'NONE', #22641, 0.1346589359789737705, 1.047197551196598075 ) ;
#19975=ADVANCED_FACE ( 'NONE', ( #36756 ), #12084, .F. ) ;
#19977=CIRCLE ( 'NONE', #40350, 0.06250000000000001388 ) ;
#19978=EDGE_LOOP ( 'NONE', ( #13557, #35128, #30712, #31509 ) ) ;
#19981=DIRECTION ( 'NONE',  ( 1.000000000000000000, -0.000000000000000000, -0.000000000000000000 ) ) ;
#19997=CARTESIAN_POINT ( 'NONE',  ( -0.2746410161513782033, -2.183180860297908144, -0.9552969701112735690 ) ) ;
#19998=EDGE_LOOP ( 'NONE', ( #29498, #14968, #39708, #16984, #32859 ) ) ;
#19999=VERTEX_POINT ( 'NONE', #28127 ) ;
#20042=ORIENTED_EDGE ( 'NONE', *, *, #38948, .T. ) ;
#20045=ORIENTED_EDGE ( 'NONE', *, *, #3599, .F. ) ;
#20054=ADVANCED_FACE ( 'NONE', ( #15089 ), #14687, .F. ) ;
#20072=VECTOR ( 'NONE', #13379, 39.37007874015748143 ) ;
#20100=DIRECTION ( 'NONE',  ( -1.000000000000000000, 0.000000000000000000, 0.000000000000000000 ) ) ;
#20123=LINE ( 'NONE', #1818, #37143 ) ;
#20167=DIRECTION ( 'NONE',  ( 0.000000000000000000, 0.000000000000000000, 1.000000000000000000 ) ) ;
#20176=DIRECTION ( 'NONE',  ( 0.000000000000000000, 0.000000000000000000, -1.000000000000000000 ) ) ;
#20192=DIRECTION ( 'NONE',  ( 0.000000000000000000, 0.000000000000000000, 1.000000000000000000 ) ) ;
#20195=VERTEX_POINT ( 'NONE', #37920 ) ;
#20196=ORIENTED_EDGE ( 'NONE', *, *, #13996, .F. ) ;
#20202=CARTESIAN_POINT ( 'NONE',  ( -0.2399999999999999079, -2.845511416290244622, -0.3415338532332813926 ) ) ;
#20206=ORIENTED_EDGE ( 'NONE', *, *, #31218, .T. ) ;
#20220=AXIS2_PLACEMENT_3D ( 'NONE', #352, #23505, #12854 ) ;
#20224=CARTESIAN_POINT ( 'NONE',  ( -0.2746410161513779258, -2.845511416290244622, -0.3415338532332813926 ) ) ;
#20237=EDGE_CURVE ( 'NONE', #22886, #20248, #6621, .T. ) ;
#20247=VERTEX_POINT ( 'NONE', #15903 ) ;
#20248=VERTEX_POINT ( 'NONE', #13219 ) ;
#20250=EDGE_LOOP ( 'NONE', ( #7347, #2568, #23293, #19393 ) ) ;
#20278=ORIENTED_EDGE ( 'NONE', *, *, #177, .T. ) ;
#20311=CYLINDRICAL_SURFACE ( 'NONE', #9271, 0.1000000000000000194 ) ;
#20323=DIRECTION ( 'NONE',  ( 1.000000000000000000, 0.000000000000000000, 0.000000000000000000 ) ) ;
#20331=CARTESIAN_POINT ( 'NONE',  ( -0.3000000000000000999, -2.183180860297908144, -0.2991170932241127844 ) ) ;
#20360=DIRECTION ( 'NONE',  ( 0.000000000000000000, 0.000000000000000000, -1.000000000000000000 ) ) ;
#20364=LINE ( 'NONE', #33491, #855 ) ;
#20371=CARTESIAN_POINT ( 'NONE',  ( -0.2399999999999999079, -2.183180860297908144, -0.4937760292030871079 ) ) ;
#20372=DIRECTION ( 'NONE',  ( 0.4999999999999997224, -0.3085698060533127451, -0.8091876635195454082 ) ) ;
#20383=VERTEX_POINT ( 'NONE', #10065 ) ;
#20393=EDGE_LOOP ( 'NONE', ( #21275, #5150, #39003, #12550 ) ) ;
#20425=ORIENTED_EDGE ( 'NONE', *, *, #39919, .F. ) ;
#20434=ORIENTED_EDGE ( 'NONE', *, *, #10505, .T. ) ;
#20437=VECTOR ( 'NONE', #37374, 39.37007874015748854 ) ;
#20440=AXIS2_PLACEMENT_3D ( 'NONE', #6092, #31419, #3220 ) ;
#20453=VERTEX_POINT ( 'NONE', #16858 ) ;
#20458=DIRECTION ( 'NONE',  ( -1.000000000000000000, 0.000000000000000000, 0.000000000000000000 ) ) ;
#20466=AXIS2_PLACEMENT_3D ( 'NONE', #5845, #21103, #8344 ) ;
#20491=DIRECTION ( 'NONE',  ( 0.000000000000000000, 0.000000000000000000, -1.000000000000000000 ) ) ;
#20496=EDGE_CURVE ( 'NONE', #8015, #7026, #16047, .T. ) ;
#20501=AXIS2_PLACEMENT_3D ( 'NONE', #1171, #16973, #4594 ) ;
#20529=AXIS2_PLACEMENT_3D ( 'NONE', #11015, #23571, #39378 ) ;
#20532=AXIS2_PLACEMENT_3D ( 'NONE', #2985, #24982, #3179 ) ;
#20545=EDGE_CURVE ( 'NONE', #30939, #22862, #19334, .T. ) ;
#20562=CYLINDRICAL_SURFACE ( 'NONE', #3556, 0.1000000000000000194 ) ;
#20565=CARTESIAN_POINT ( 'NONE',  ( -0.2746410161513776482, -4.121841830394775030, -0.5449218438908057793 ) ) ;
#20569=DIRECTION ( 'NONE',  ( 1.000000000000000000, 0.000000000000000000, 0.000000000000000000 ) ) ;
#20574=DIRECTION ( 'NONE',  ( 0.000000000000000000, 0.000000000000000000, -1.000000000000000000 ) ) ;
#20576=CIRCLE ( 'NONE', #21902, 0.4615209409081865166 ) ;
#20577=FACE_OUTER_BOUND ( 'NONE', #32423, .T. ) ;
#20591=AXIS2_PLACEMENT_3D ( 'NONE', #33819, #24359, #27645 ) ;
#20593=VERTEX_POINT ( 'NONE', #29799 ) ;
#20599=ORIENTED_EDGE ( 'NONE', *, *, #5903, .F. ) ;
#20611=ORIENTED_EDGE ( 'NONE', *, *, #16072, .F. ) ;
#20617=DIRECTION ( 'NONE',  ( 0.000000000000000000, -5.463695987328525648E-15, -1.000000000000000000 ) ) ;
#20626=DIRECTION ( 'NONE',  ( 0.000000000000000000, 0.000000000000000000, -1.000000000000000000 ) ) ;
#20633=CIRCLE ( 'NONE', #2883, 0.1000000000000000194 ) ;
#20658=DIRECTION ( 'NONE',  ( -0.4999999999999946709, 0.3297230132044422501, 0.8008013077932555346 ) ) ;
#20661=ORIENTED_EDGE ( 'NONE', *, *, #35593, .T. ) ;
#20664=AXIS2_PLACEMENT_3D ( 'NONE', #27493, #33644, #32693 ) ;
#20679=AXIS2_PLACEMENT_3D ( 'NONE', #37812, #10031, #22202 ) ;
#20684=VECTOR ( 'NONE', #19027, 39.37007874015748143 ) ;
#20692=VECTOR ( 'NONE', #17527, 39.37007874015748854 ) ;
#20712=ORIENTED_EDGE ( 'NONE', *, *, #29774, .T. ) ;
#20713=CIRCLE ( 'NONE', #1041, 0.1000000000000000194 ) ;
#20724=CIRCLE ( 'NONE', #22701, 0.1000000000000000194 ) ;
#20728=LINE ( 'NONE', #18421, #22499 ) ;
#20741=CIRCLE ( 'NONE', #8883, 0.1000000000000000194 ) ;
#20743=FACE_OUTER_BOUND ( 'NONE', #38946, .T. ) ;
#20744=EDGE_CURVE ( 'NONE', #26629, #24814, #2244, .T. ) ;
#20761=VERTEX_POINT ( 'NONE', #2235 ) ;
#20779=DIRECTION ( 'NONE',  ( 0.000000000000000000, -0.8438867430782092116, -0.5365213554527465956 ) ) ;
#20784=EDGE_CURVE ( 'NONE', #40011, #38034, #21568, .T. ) ;
#20785=DIRECTION ( 'NONE',  ( -0.4999999999999991118, -0.1289820025937478687, -0.8563665354314745626 ) ) ;
#20791=EDGE_CURVE ( 'NONE', #34047, #26723, #17987, .T. ) ;
#20793=EDGE_CURVE ( 'NONE', #20761, #14767, #8794, .T. ) ;
#20801=ORIENTED_EDGE ( 'NONE', *, *, #7983, .T. ) ;
#20807=DIRECTION ( 'NONE',  ( 1.000000000000000000, 0.000000000000000000, 0.000000000000000000 ) ) ;
#20809=CARTESIAN_POINT ( 'NONE',  ( -0.2399999999999999079, -4.350369088120884520, -0.8413950570247814564 ) ) ;
#20827=DIRECTION ( 'NONE',  ( 1.000000000000000000, 0.000000000000000000, 0.000000000000000000 ) ) ;
#20831=VECTOR ( 'NONE', #16524, 39.37007874015748854 ) ;
#20833=FACE_BOUND ( 'NONE', #21189, .T. ) ;
#20834=DIRECTION ( 'NONE',  ( 0.000000000000000000, 0.000000000000000000, -1.000000000000000000 ) ) ;
#20863=ORIENTED_EDGE ( 'NONE', *, *, #37288, .F. ) ;
#20866=LINE ( 'NONE', #1937, #32896 ) ;
#20896=CARTESIAN_POINT ( 'NONE',  ( -0.2399999999999999079, -3.941790907013290823, -0.4084369376873030477 ) ) ;
#20908=DIRECTION ( 'NONE',  ( 0.000000000000000000, 0.000000000000000000, -1.000000000000000000 ) ) ;
#20913=DIRECTION ( 'NONE',  ( 1.000000000000000000, -0.000000000000000000, -0.000000000000000000 ) ) ;
#20955=VERTEX_POINT ( 'NONE', #3829 ) ;
#20965=LINE ( 'NONE', #8588, #17496 ) ;
#20968=ADVANCED_FACE ( 'NONE', ( #22375 ), #792, .T. ) ;
#20969=ORIENTED_EDGE ( 'NONE', *, *, #38693, .T. ) ;
#20995=DIRECTION ( 'NONE',  ( 0.8660254037844378194, -0.3535533905932747856, 0.3535533905932747856 ) ) ;
#21000=ORIENTED_EDGE ( 'NONE', *, *, #35990, .T. ) ;
#21013=ADVANCED_FACE ( 'NONE', ( #31615 ), #19284, .T. ) ;
#21021=FACE_BOUND ( 'NONE', #8022, .T. ) ;
#21048=EDGE_CURVE ( 'NONE', #27585, #28698, #36404, .T. ) ;
#21055=ORIENTED_EDGE ( 'NONE', *, *, #28029, .F. ) ;
#21074=CARTESIAN_POINT ( 'NONE',  ( -0.2399999999999999079, -3.745280840418592661, 0.04438736989695814955 ) ) ;
#21085=EDGE_CURVE ( 'NONE', #20761, #36543, #18024, .T. ) ;
#21087=VECTOR ( 'NONE', #9850, 39.37007874015748143 ) ;
#21103=DIRECTION ( 'NONE',  ( -1.000000000000000000, -0.000000000000000000, -0.000000000000000000 ) ) ;
#21104=ORIENTED_EDGE ( 'NONE', *, *, #23350, .F. ) ;
#21118=AXIS2_PLACEMENT_3D ( 'NONE', #17687, #33327, #11321 ) ;
#21121=CARTESIAN_POINT ( 'NONE',  ( -0.2399999999999999079, -2.377368549242099949, -0.4802393080720198104 ) ) ;
#21122=CARTESIAN_POINT ( 'NONE',  ( -0.2746410161513782033, -2.003129936916423048, -0.4197911229995844873 ) ) ;
#21137=VERTEX_POINT ( 'NONE', #39403 ) ;
#21159=DIRECTION ( 'NONE',  ( 0.000000000000000000, 0.5365213554527469286, -0.8438867430782091006 ) ) ;
#21165=ORIENTED_EDGE ( 'NONE', *, *, #34368, .F. ) ;
#21171=CARTESIAN_POINT ( 'NONE',  ( -0.3000000000000000999, -1.739646749720735741, -0.3661865639197241507 ) ) ;
#21176=VECTOR ( 'NONE', #13590, 39.37007874015748143 ) ;
#21186=DIRECTION ( 'NONE',  ( 0.000000000000000000, -0.7071067811865474617, -0.7071067811865474617 ) ) ;
#21189=EDGE_LOOP ( 'NONE', ( #10468, #12237, #1141, #38785, #38652, #17104, #9015, #25811, #23511 ) ) ;
#21200=CIRCLE ( 'NONE', #36959, 0.1000000000000000194 ) ;
#21203=EDGE_CURVE ( 'NONE', #17501, #26475, #32816, .T. ) ;
#21205=FACE_OUTER_BOUND ( 'NONE', #33642, .T. ) ;
#21211=VERTEX_POINT ( 'NONE', #1380 ) ;
#21219=VECTOR ( 'NONE', #28901, 39.37007874015748143 ) ;
#21220=LINE ( 'NONE', #37043, #29713 ) ;
#21224=DIRECTION ( 'NONE',  ( 1.000000000000000000, 0.000000000000000000, 0.000000000000000000 ) ) ;
#21241=AXIS2_PLACEMENT_3D ( 'NONE', #23066, #29015, #32905 ) ;
#21254=ORIENTED_EDGE ( 'NONE', *, *, #32789, .F. ) ;
#21263=CIRCLE ( 'NONE', #3518, 0.1000000000000000194 ) ;
#21275=ORIENTED_EDGE ( 'NONE', *, *, #13039, .F. ) ;
#21301=CARTESIAN_POINT ( 'NONE',  ( -0.3000000000000000999, -2.861028283584748699, -0.4103205306338890690 ) ) ;
#21302=EDGE_LOOP ( 'NONE', ( #32308, #4389, #34662, #10941 ) ) ;
#21319=EDGE_LOOP ( 'NONE', ( #14873, #29633, #11744, #32248 ) ) ;
#21322=DIRECTION ( 'NONE',  ( 0.000000000000000000, 0.5781348229923771731, -0.8159412518334715481 ) ) ;
#21326=DIRECTION ( 'NONE',  ( 0.000000000000000000, 0.000000000000000000, 1.000000000000000000 ) ) ;
#21329=ORIENTED_EDGE ( 'NONE', *, *, #8544, .T. ) ;
#21345=AXIS2_PLACEMENT_3D ( 'NONE', #21645, #33979, #25127 ) ;
#21355=CARTESIAN_POINT ( 'NONE',  ( -0.2399999999999999079, -1.835749455202394298, -0.3938319975228649072 ) ) ;
#21357=VECTOR ( 'NONE', #5052, 39.37007874015748143 ) ;
#21376=EDGE_CURVE ( 'NONE', #23612, #17567, #23297, .T. ) ;
#21379=LINE ( 'NONE', #14980, #4660 ) ;
#21408=VECTOR ( 'NONE', #28410, 39.37007874015748143 ) ;
#21419=ORIENTED_EDGE ( 'NONE', *, *, #25626, .T. ) ;
#21424=AXIS2_PLACEMENT_3D ( 'NONE', #40051, #24443, #9398 ) ;
#21426=ORIENTED_EDGE ( 'NONE', *, *, #21604, .F. ) ;
#21444=CARTESIAN_POINT ( 'NONE',  ( -0.2399999999999999079, -2.183180860297908144, -0.4937760292030871079 ) ) ;
#21474=DIRECTION ( 'NONE',  ( 0.000000000000000000, 0.000000000000000000, -1.000000000000000000 ) ) ;
#21479=ADVANCED_FACE ( 'NONE', ( #29646 ), #12435, .F. ) ;
#21482=EDGE_CURVE ( 'NONE', #18572, #2349, #22138, .T. ) ;
#21493=EDGE_CURVE ( 'NONE', #4130, #9666, #36440, .T. ) ;
#21495=DIRECTION ( 'NONE',  ( -1.000000000000000000, 0.000000000000000000, 0.000000000000000000 ) ) ;
#21529=ORIENTED_EDGE ( 'NONE', *, *, #25390, .T. ) ;
#21533=LINE ( 'NONE', #30965, #3337 ) ;
#21538=ADVANCED_FACE ( 'NONE', ( #21205 ), #10841, .F. ) ;
#21556=CARTESIAN_POINT ( 'NONE',  ( -0.2746410161513779258, -2.377368549242099949, -0.4802393080720198104 ) ) ;
#21558=DIRECTION ( 'NONE',  ( 0.000000000000000000, -0.7071067811865484609, 0.7071067811865465735 ) ) ;
#21568=LINE ( 'NONE', #30612, #35732 ) ;
#21588=DIRECTION ( 'NONE',  ( 0.8660254037844395958, 0.2890674114961868102, -0.4079706259167349969 ) ) ;
#21592=CARTESIAN_POINT ( 'NONE',  ( -0.2399999999999999079, -2.026158573466832813, -0.3155405389364159263 ) ) ;
#21604=EDGE_CURVE ( 'NONE', #1766, #9912, #30061, .T. ) ;
#21606=PLANE ( 'NONE',  #18624 ) ;
#21617=VERTEX_POINT ( 'NONE', #27783 ) ;
#21632=DIRECTION ( 'NONE',  ( 1.000000000000000000, 0.000000000000000000, 0.000000000000000000 ) ) ;
#21645=CARTESIAN_POINT ( 'NONE',  ( -0.2399999999999999079, -1.835749455202394298, -0.3938319975228649072 ) ) ;
#21652=DIRECTION ( 'NONE',  ( 0.000000000000000000, 0.000000000000000000, -1.000000000000000000 ) ) ;
#21658=ORIENTED_EDGE ( 'NONE', *, *, #25741, .T. ) ;
#21677=DIRECTION ( 'NONE',  ( 0.000000000000000000, 0.000000000000000000, -1.000000000000000000 ) ) ;
#21694=CARTESIAN_POINT ( 'NONE',  ( -0.2399999999999999079, -2.183180860297908144, -0.2991170932241127844 ) ) ;
#21725=CARTESIAN_POINT ( 'NONE',  ( -0.2399999999999999079, -1.804235510932644004, -0.1101860188971505033 ) ) ;
#21731=AXIS2_PLACEMENT_3D ( 'NONE', #30852, #24486, #37020 ) ;
#21732=EDGE_CURVE ( 'NONE', #3317, #31622, #14769, .T. ) ;
#21740=DIRECTION ( 'NONE',  ( -1.000000000000000000, -0.000000000000000000, -0.000000000000000000 ) ) ;
#21742=SHAPE_REPRESENTATION ( 'Cage Hanger', ( #27819 ), #33713 ) ;
#21765=ORIENTED_EDGE ( 'NONE', *, *, #39336, .T. ) ;
#21780=EDGE_LOOP ( 'NONE', ( #9101, #28913, #9508, #38450 ) ) ;
#21783=FACE_OUTER_BOUND ( 'NONE', #23587, .T. ) ;
#21800=CARTESIAN_POINT ( 'NONE',  ( -0.2399999999999999079, -4.121841830394775030, -0.5449218438908057793 ) ) ;
#21802=EDGE_CURVE ( 'NONE', #31054, #21617, #15600, .T. ) ;
#21803=CARTESIAN_POINT ( 'NONE',  ( -0.2399999999999999079, -4.176085227118957022, -0.6840180543573738392 ) ) ;
#21811=DIRECTION ( 'NONE',  ( -1.000000000000000000, -0.000000000000000000, -0.000000000000000000 ) ) ;
#21831=LINE ( 'NONE', #37250, #24431 ) ;
#21836=EDGE_CURVE ( 'NONE', #12108, #35653, #31239, .T. ) ;
#21846=DIRECTION ( 'NONE',  ( 0.000000000000000000, 0.000000000000000000, 1.000000000000000000 ) ) ;
#21854=EDGE_CURVE ( 'NONE', #19589, #9095, #24451, .T. ) ;
#21870=EDGE_LOOP ( 'NONE', ( #6208, #17965, #11592, #38000 ) ) ;
#21895=CONICAL_SURFACE ( 'NONE', #21241, 0.1600000000000007527, 1.047197551196599186 ) ;
#21897=DIRECTION ( 'NONE',  ( 0.4999999999999991673, -0.1289820025937439552, -0.8563665354314752287 ) ) ;
#21902=AXIS2_PLACEMENT_3D ( 'NONE', #25678, #35339, #22205 ) ;
#21916=ORIENTED_EDGE ( 'NONE', *, *, #2660, .F. ) ;
#21921=DIRECTION ( 'NONE',  ( 0.000000000000000000, 0.000000000000000000, -1.000000000000000000 ) ) ;
#21960=EDGE_LOOP ( 'NONE', ( #31109, #14725, #28240, #34082 ) ) ;
#21961=CARTESIAN_POINT ( 'NONE',  ( -0.2746410161513779258, -3.291368864184588183, -0.6988176298300771139 ) ) ;
#21964=DIRECTION ( 'NONE',  ( 1.000000000000000000, 0.000000000000000000, 0.000000000000000000 ) ) ;
#21966=ORIENTED_EDGE ( 'NONE', *, *, #32337, .F. ) ;
#21980=CIRCLE ( 'NONE', #10125, 0.09999999999999999167 ) ;
#21981=VECTOR ( 'NONE', #31008, 39.37007874015748143 ) ;
#21991=EDGE_CURVE ( 'NONE', #20248, #36967, #13175, .T. ) ;
#21993=ORIENTED_EDGE ( 'NONE', *, *, #30750, .F. ) ;
#22004=DIRECTION ( 'NONE',  ( 0.000000000000000000, 3.414809992080312950E-15, -1.000000000000000000 ) ) ;
#22014=DIRECTION ( 'NONE',  ( 0.000000000000000000, 0.9246857012436752177, -0.3807313408632033713 ) ) ;
#22024=AXIS2_PLACEMENT_3D ( 'NONE', #12933, #38018, #35139 ) ;
#22034=VERTEX_POINT ( 'NONE', #5666 ) ;
#22073=DIRECTION ( 'NONE',  ( -0.000000000000000000, 0.7071067811865474617, 0.7071067811865474617 ) ) ;
#22099=DIRECTION ( 'NONE',  ( -1.000000000000000000, -0.000000000000000000, -0.000000000000000000 ) ) ;
#22110=EDGE_CURVE ( 'NONE', #23675, #22635, #12444, .T. ) ;
#22113=CIRCLE ( 'NONE', #29344, 0.1946589359789743512 ) ;
#22121=ADVANCED_FACE ( 'NONE', ( #11837 ), #19761, .T. ) ;
#22138=LINE ( 'NONE', #15930, #20684 ) ;
#22159=CARTESIAN_POINT ( 'NONE',  ( -0.2746410161513782033, -1.891808285041389093, -0.4498908273618595910 ) ) ;
#22169=DIRECTION ( 'NONE',  ( 1.000000000000000000, 0.000000000000000000, 0.000000000000000000 ) ) ;
#22178=FACE_OUTER_BOUND ( 'NONE', #345, .T. ) ;
#22182=CARTESIAN_POINT ( 'NONE',  ( -0.2399999999999999079, -3.849534981189179028, -0.1910928155360645808 ) ) ;
#22202=DIRECTION ( 'NONE',  ( 0.000000000000000000, 0.000000000000000000, -1.000000000000000000 ) ) ;
#22205=DIRECTION ( 'NONE',  ( 0.000000000000000000, 0.000000000000000000, -1.000000000000000000 ) ) ;
#22206=PLANE ( 'NONE',  #16748 ) ;
#22230=EDGE_CURVE ( 'NONE', #19587, #27977, #21533, .T. ) ;
#22238=ORIENTED_EDGE ( 'NONE', *, *, #5674, .T. ) ;
#22280=ORIENTED_EDGE ( 'NONE', *, *, #35305, .F. ) ;
#22281=ORIENTED_EDGE ( 'NONE', *, *, #23378, .T. ) ;
#22286=LINE ( 'NONE', #12594, #34285 ) ;
#22292=ADVANCED_FACE ( 'NONE', ( #40383 ), #5203, .F. ) ;
#22344=LINE ( 'NONE', #9155, #17993 ) ;
#22360=CARTESIAN_POINT ( 'NONE',  ( -0.2746410161513779258, -2.423474325126674156, -0.5576739111151496342 ) ) ;
#22369=ORIENTED_EDGE ( 'NONE', *, *, #16291, .F. ) ;
#22371=DIRECTION ( 'NONE',  ( -0.4999999999999952816, 0.7066258520834667323, 0.5006794435238172136 ) ) ;
#22375=FACE_OUTER_BOUND ( 'NONE', #10477, .T. ) ;
#22378=VERTEX_POINT ( 'NONE', #526 ) ;
#22395=FACE_OUTER_BOUND ( 'NONE', #34105, .T. ) ;
#22402=DIRECTION ( 'NONE',  ( -1.000000000000000000, -0.000000000000000000, -0.000000000000000000 ) ) ;
#22480=VECTOR ( 'NONE', #2857, 39.37007874015748143 ) ;
#22482=CIRCLE ( 'NONE', #2088, 0.1000000000000000194 ) ;
#22494=CARTESIAN_POINT ( 'NONE',  ( -0.3000000000000000999, -3.751862894713570817, -0.4282819086714443890 ) ) ;
#22499=VECTOR ( 'NONE', #36946, 39.37007874015748854 ) ;
#22507=CIRCLE ( 'NONE', #23829, 0.1346589359789726881 ) ;
#22511=CARTESIAN_POINT ( 'NONE',  ( -0.2399999999999999079, -3.941790907013290823, -0.4709369376873030477 ) ) ;
#22516=CYLINDRICAL_SURFACE ( 'NONE', #28269, 0.1000000000000000056 ) ;
#22528=DIRECTION ( 'NONE',  ( 0.000000000000000000, -0.3563057211773426602, -0.9343694307158671997 ) ) ;
#22533=ORIENTED_EDGE ( 'NONE', *, *, #31662, .T. ) ;
#22534=ADVANCED_FACE ( 'NONE', ( #29261 ), #32943, .F. ) ;
#22539=AXIS2_PLACEMENT_3D ( 'NONE', #30597, #14341, #11258 ) ;
#22552=EDGE_CURVE ( 'NONE', #24406, #40516, #125, .T. ) ;
#22565=VECTOR ( 'NONE', #30389, 39.37007874015748854 ) ;
#22566=CONICAL_SURFACE ( 'NONE', #27168, 0.1600000000000007527, 1.047197551196599186 ) ;
#22606=PRODUCT_DEFINITION_SHAPE ( 'NONE', 'NONE',  #40563 ) ;
#22635=VERTEX_POINT ( 'NONE', #4847 ) ;
#22641=AXIS2_PLACEMENT_3D ( 'NONE', #26743, #17262, #20167 ) ;
#22659=CYLINDRICAL_SURFACE ( 'NONE', #10644, 0.1000000000000000194 ) ;
#22669=FACE_OUTER_BOUND ( 'NONE', #24491, .T. ) ;
#22675=DIRECTION ( 'NONE',  ( 0.000000000000000000, 0.9343694307158671997, -0.3563057211773426602 ) ) ;
#22678=DIRECTION ( 'NONE',  ( 0.000000000000000000, 0.000000000000000000, -1.000000000000000000 ) ) ;
#22701=AXIS2_PLACEMENT_3D ( 'NONE', #37663, #25339, #12369 ) ;
#22713=AXIS2_PLACEMENT_3D ( 'NONE', #4310, #23048, #1451 ) ;
#22722=CARTESIAN_POINT ( 'NONE',  ( -0.2399999999999999079, -4.289222312108804225, -0.7308809693675260011 ) ) ;
#22729=DIRECTION ( 'NONE',  ( 0.000000000000000000, -0.5781348229923763959, 0.8159412518334722142 ) ) ;
#22735=VERTEX_POINT ( 'NONE', #29978 ) ;
#22745=ADVANCED_FACE ( 'NONE', ( #10852 ), #20311, .T. ) ;
#22772=VECTOR ( 'NONE', #16262, 39.37007874015748143 ) ;
#22779=EDGE_LOOP ( 'NONE', ( #32224, #22963, #6202, #608 ) ) ;
#22782=FACE_OUTER_BOUND ( 'NONE', #30239, .T. ) ;
#22783=CARTESIAN_POINT ( 'NONE',  ( -0.2399999999999999079, -1.804235510932644004, -0.05018601889714981862 ) ) ;
#22840=ORIENTED_EDGE ( 'NONE', *, *, #32376, .T. ) ;
#22841=ORIENTED_EDGE ( 'NONE', *, *, #13249, .F. ) ;
#22855=VERTEX_POINT ( 'NONE', #11371 ) ;
#22862=VERTEX_POINT ( 'NONE', #30501 ) ;
#22882=DIRECTION ( 'NONE',  ( -1.000000000000000000, -0.000000000000000000, -0.000000000000000000 ) ) ;
#22886=VERTEX_POINT ( 'NONE', #1744 ) ;
#22888=EDGE_CURVE ( 'NONE', #36123, #9809, #11589, .T. ) ;
#22894=ORIENTED_EDGE ( 'NONE', *, *, #2442, .T. ) ;
#22923=DIRECTION ( 'NONE',  ( 0.000000000000000000, 0.000000000000000000, -1.000000000000000000 ) ) ;
#22940=ORIENTED_EDGE ( 'NONE', *, *, #9491, .F. ) ;
#22948=ORIENTED_EDGE ( 'NONE', *, *, #7608, .F. ) ;
#22963=ORIENTED_EDGE ( 'NONE', *, *, #20545, .F. ) ;
#22992=ORIENTED_EDGE ( 'NONE', *, *, #5418, .F. ) ;
#23002=EDGE_CURVE ( 'NONE', #28698, #18572, #10592, .T. ) ;
#23027=CARTESIAN_POINT ( 'NONE',  ( -0.3000000000000000999, -3.334889855281614857, -0.6641625420049475093 ) ) ;
#23031=CARTESIAN_POINT ( 'NONE',  ( -0.2399999999999999079, -3.840189043187996809, -0.1239867222638698224 ) ) ;
#23044=ORIENTED_EDGE ( 'NONE', *, *, #30840, .F. ) ;
#23048=DIRECTION ( 'NONE',  ( 1.000000000000000000, 0.000000000000000000, 0.000000000000000000 ) ) ;
#23056=CYLINDRICAL_SURFACE ( 'NONE', #29219, 0.4615209409081864611 ) ;
#23066=CARTESIAN_POINT ( 'NONE',  ( -0.2399999999999999079, -2.511040369707300268, -0.4948468226404901804 ) ) ;
#23074=DIRECTION ( 'NONE',  ( 0.000000000000000000, -0.8159412518334726583, -0.5781348229923756188 ) ) ;
#23088=CARTESIAN_POINT ( 'NONE',  ( -0.2399999999999999079, -2.853330612949663170, -0.7088139570729240502 ) ) ;
#23096=CARTESIAN_POINT ( 'NONE',  ( -0.3000000000000000999, -2.861028283584748699, -0.4103205306338890690 ) ) ;
#23100=CARTESIAN_POINT ( 'NONE',  ( -0.2399999999999999079, -2.853330612949663170, -0.6088139570729240724 ) ) ;
#23112=( NAMED_UNIT ( * ) SI_UNIT ( $, .STERADIAN. ) SOLID_ANGLE_UNIT ( ) );
#23154=CARTESIAN_POINT ( 'NONE',  ( -0.3000000000000000999, -2.289343986263487896, -0.7686455968847020204 ) ) ;
#23159=EDGE_CURVE ( 'NONE', #1199, #28968, #16507, .T. ) ;
#23175=VECTOR ( 'NONE', #161, 39.37007874015748143 ) ;
#23181=AXIS2_PLACEMENT_3D ( 'NONE', #4268, #20323, #4862 ) ;
#23200=ORIENTED_EDGE ( 'NONE', *, *, #32605, .F. ) ;
#23210=CONICAL_SURFACE ( 'NONE', #4150, 0.1346589359789736318, 1.047197551196598742 ) ;
#23223=CYLINDRICAL_SURFACE ( 'NONE', #19875, 0.1946589359789742957 ) ;
#23231=ORIENTED_EDGE ( 'NONE', *, *, #17805, .T. ) ;
#23237=VECTOR ( 'NONE', #38732, 39.37007874015748854 ) ;
#23256=LINE ( 'NONE', #36177, #319 ) ;
#23276=AXIS2_PLACEMENT_3D ( 'NONE', #12092, #9397, #40050 ) ;
#23283=CIRCLE ( 'NONE', #4857, 0.1600000000000006140 ) ;
#23285=AXIS2_PLACEMENT_3D ( 'NONE', #25069, #22402, #22004 ) ;
#23292=ORIENTED_EDGE ( 'NONE', *, *, #4175, .F. ) ;
#23293=ORIENTED_EDGE ( 'NONE', *, *, #26543, .F. ) ;
#23297=LINE ( 'NONE', #6653, #33831 ) ;
#23301=CIRCLE ( 'NONE', #37753, 0.06250000000000001388 ) ;
#23306=EDGE_CURVE ( 'NONE', #12532, #24285, #12897, .T. ) ;
#23341=DIRECTION ( 'NONE',  ( 0.000000000000000000, 0.000000000000000000, 1.000000000000000000 ) ) ;
#23350=EDGE_CURVE ( 'NONE', #478, #40377, #4709, .T. ) ;
#23354=LINE ( 'NONE', #14662, #28533 ) ;
#23367=ORIENTED_EDGE ( 'NONE', *, *, #17306, .T. ) ;
#23378=EDGE_CURVE ( 'NONE', #23675, #29082, #31604, .T. ) ;
#23392=CARTESIAN_POINT ( 'NONE',  ( -0.2399999999999999079, -2.427691829037316396, -0.9241619397096791921 ) ) ;
#23397=AXIS2_PLACEMENT_3D ( 'NONE', #33543, #21224, #33761 ) ;
#23398=DIMENSIONAL_EXPONENTS ( 1.000000000000000000, 0.000000000000000000, 0.000000000000000000, 0.000000000000000000, 0.000000000000000000, 0.000000000000000000, 0.000000000000000000 ) ;
#23425=CARTESIAN_POINT ( 'NONE',  ( -0.2399999999999999079, -2.845511416290244622, -0.3415338532332813926 ) ) ;
#23439=DIRECTION ( 'NONE',  ( 0.000000000000000000, 0.7071067811865474617, 0.7071067811865475727 ) ) ;
#23444=CARTESIAN_POINT ( 'NONE',  ( -0.3000000000000000999, -1.962518963160043706, -0.3791801492432049225 ) ) ;
#23450=CYLINDRICAL_SURFACE ( 'NONE', #11849, 0.4615209409081864611 ) ;
#23477=CARTESIAN_POINT ( 'NONE',  ( -0.2399999999999999079, -2.909786385774835171, -0.3705357231075770419 ) ) ;
#23494=CARTESIAN_POINT ( 'NONE',  ( -0.2746410161513776482, -3.941790907013290823, -0.4709369376873030477 ) ) ;
#23505=DIRECTION ( 'NONE',  ( -1.000000000000000000, 0.000000000000000000, 0.000000000000000000 ) ) ;
#23507=LINE ( 'NONE', #23088, #31215 ) ;
#23511=ORIENTED_EDGE ( 'NONE', *, *, #28029, .T. ) ;
#23523=DIRECTION ( 'NONE',  ( 0.000000000000000000, -5.463695987328525648E-15, -1.000000000000000000 ) ) ;
#23526=LINE ( 'NONE', #32749, #28632 ) ;
#23534=ADVANCED_FACE ( 'NONE', ( #22782 ), #13289, .F. ) ;
#23538=DIRECTION ( 'NONE',  ( 0.4379975771764356707, -0.8989761522908004121, 0.000000000000000000 ) ) ;
#23571=DIRECTION ( 'NONE',  ( -1.000000000000000000, -0.000000000000000000, -0.000000000000000000 ) ) ;
#23575=EDGE_CURVE ( 'NONE', #10025, #35098, #30980, .T. ) ;
#23587=EDGE_LOOP ( 'NONE', ( #38232, #1056, #6907, #40529 ) ) ;
#23591=CARTESIAN_POINT ( 'NONE',  ( -0.2399999999999999079, -2.761122741982423801, -0.2878817176880067996 ) ) ;
#23599=EDGE_CURVE ( 'NONE', #12802, #16220, #22482, .T. ) ;
#23602=CARTESIAN_POINT ( 'NONE',  ( -0.2399999999999999079, -4.289222312108804225, -0.5708809693675255259 ) ) ;
#23603=ADVANCED_FACE ( 'NONE', ( #33986 ), #4039, .F. ) ;
#23612=VERTEX_POINT ( 'NONE', #24329 ) ;
#23626=EDGE_CURVE ( 'NONE', #36543, #12532, #28033, .T. ) ;
#23631=LINE ( 'NONE', #16423, #19305 ) ;
#23664=FACE_OUTER_BOUND ( 'NONE', #37201, .T. ) ;
#23675=VERTEX_POINT ( 'NONE', #31110 ) ;
#23682=ORIENTED_EDGE ( 'NONE', *, *, #5622, .T. ) ;
#23694=VERTEX_POINT ( 'NONE', #5590 ) ;
#23695=VERTEX_POINT ( 'NONE', #12380 ) ;
#23706=DIRECTION ( 'NONE',  ( 0.000000000000000000, 0.000000000000000000, -1.000000000000000000 ) ) ;
#23721=CARTESIAN_POINT ( 'NONE',  ( -0.2399999999999999079, -2.139295658456680904, -0.3624034539465684213 ) ) ;
#23728=APPLICATION_CONTEXT ( 'configuration controlled 3d designs of mechanical parts and assemblies' ) ;
#23733=CONICAL_SURFACE ( 'NONE', #14523, 0.1600000000000006417, 1.047197551196599408 ) ;
#23764=AXIS2_PLACEMENT_3D ( 'NONE', #12344, #3695, #9450 ) ;
#23767=AXIS2_PLACEMENT_3D ( 'NONE', #4241, #35715, #26466 ) ;
#23774=EDGE_LOOP ( 'NONE', ( #13609, #16161, #964, #24345 ) ) ;
#23786=FACE_OUTER_BOUND ( 'NONE', #37350, .T. ) ;
#23789=CARTESIAN_POINT ( 'NONE',  ( -0.2746410161513779258, -2.139295658456680904, -0.2024034539465678073 ) ) ;
#23795=ORIENTED_EDGE ( 'NONE', *, *, #38693, .F. ) ;
#23796=EDGE_CURVE ( 'NONE', #25380, #22378, #37891, .T. ) ;
#23799=CARTESIAN_POINT ( 'NONE',  ( -0.3000000000000000999, -2.377058624452622393, -0.8919706583825134372 ) ) ;
#23821=EDGE_CURVE ( 'NONE', #24506, #34622, #29021, .T. ) ;
#23829=AXIS2_PLACEMENT_3D ( 'NONE', #11343, #20827, #2086 ) ;
#23830=CIRCLE ( 'NONE', #24497, 0.1000000000000000194 ) ;
#23833=CARTESIAN_POINT ( 'NONE',  ( -0.2399999999999999079, -1.891808285041389093, -0.4498908273618595910 ) ) ;
#23872=DIRECTION ( 'NONE',  ( -1.000000000000000000, -0.000000000000000000, -0.000000000000000000 ) ) ;
#23879=CARTESIAN_POINT ( 'NONE',  ( -0.2746410161513776482, -4.289222312108804225, -0.5708809693675255259 ) ) ;
#23882=FACE_OUTER_BOUND ( 'NONE', #1598, .T. ) ;
#23887=VECTOR ( 'NONE', #9227, 39.37007874015748143 ) ;
#23891=CARTESIAN_POINT ( 'NONE',  ( -0.2746410161513770931, -3.220869926774937664, -0.5656276768926112863 ) ) ;
#23895=VERTEX_POINT ( 'NONE', #31500 ) ;
#23924=DIRECTION ( 'NONE',  ( -1.000000000000000000, -0.000000000000000000, -0.000000000000000000 ) ) ;
#23940=ORIENTED_EDGE ( 'NONE', *, *, #661, .T. ) ;
#23944=EDGE_LOOP ( 'NONE', ( #38144, #31510, #27126, #33735, #34203 ) ) ;
#23948=AXIS2_PLACEMENT_3D ( 'NONE', #3226, #15775, #31824 ) ;
#23952=LINE ( 'NONE', #17356, #13440 ) ;
#23976=CIRCLE ( 'NONE', #18706, 0.1000000000000000194 ) ;
#23984=CARTESIAN_POINT ( 'NONE',  ( -0.3000000000000000999, -2.945416957892569521, -0.4639726661791638840 ) ) ;
#23989=EDGE_LOOP ( 'NONE', ( #21329, #34901, #37733, #27276 ) ) ;
#24005=AXIS2_PLACEMENT_3D ( 'NONE', #23154, #17373, #14077 ) ;
#24019=ORIENTED_EDGE ( 'NONE', *, *, #37818, .F. ) ;
#24032=AXIS2_PLACEMENT_3D ( 'NONE', #20565, #38662, #13964 ) ;
#24034=CIRCLE ( 'NONE', #29929, 0.6115209409081865388 ) ;
#24036=DIRECTION ( 'NONE',  ( -0.4999999999999968359, 0.4646411234949411884, -0.7308273574226419322 ) ) ;
#24089=DIRECTION ( 'NONE',  ( 0.4999999999999985567, 0.4646411234949399116, -0.7308273574226413771 ) ) ;
#24103=ORIENTED_EDGE ( 'NONE', *, *, #4125, .F. ) ;
#24111=CARTESIAN_POINT ( 'NONE',  ( -0.2399999999999999079, -4.289222312108804225, -0.5708809693675255259 ) ) ;
#24113=CARTESIAN_POINT ( 'NONE',  ( -0.2399999999999999079, -3.791721498889941255, -0.2726869407194119077 ) ) ;
#24159=DIRECTION ( 'NONE',  ( 1.000000000000000000, 0.000000000000000000, 0.000000000000000000 ) ) ;
#24189=DIRECTION ( 'NONE',  ( -1.000000000000000000, 0.000000000000000000, 0.000000000000000000 ) ) ;
#24212=ORIENTED_EDGE ( 'NONE', *, *, #9486, .F. ) ;
#24242=ORIENTED_EDGE ( 'NONE', *, *, #34392, .T. ) ;
#24249=EDGE_CURVE ( 'NONE', #9331, #22862, #12957, .T. ) ;
#24259=ADVANCED_FACE ( 'NONE', ( #37843 ), #9657, .T. ) ;
#24260=DIRECTION ( 'NONE',  ( 1.000000000000000000, 0.000000000000000000, 0.000000000000000000 ) ) ;
#24279=ADVANCED_FACE ( 'NONE', ( #30001 ), #23450, .F. ) ;
#24281=DIRECTION ( 'NONE',  ( 0.000000000000000000, 0.000000000000000000, -1.000000000000000000 ) ) ;
#24285=VERTEX_POINT ( 'NONE', #32862 ) ;
#24289=CARTESIAN_POINT ( 'NONE',  ( -0.3000000000000000999, -2.139295658456680904, -0.2024034539465678073 ) ) ;
#24293=ORIENTED_EDGE ( 'NONE', *, *, #34569, .T. ) ;
#24312=CARTESIAN_POINT ( 'NONE',  ( -0.2399999999999999079, -3.433273040916029029, -1.270777394095183199 ) ) ;
#24325=EDGE_CURVE ( 'NONE', #9243, #8729, #16434, .T. ) ;
#24329=CARTESIAN_POINT ( 'NONE',  ( -0.2399999999999999079, -4.292451985131092940, -0.8428112192407016812 ) ) ;
#24345=ORIENTED_EDGE ( 'NONE', *, *, #6399, .T. ) ;
#24353=ORIENTED_EDGE ( 'NONE', *, *, #27363, .T. ) ;
#24354=ORIENTED_EDGE ( 'NONE', *, *, #26532, .F. ) ;
#24355=ADVANCED_FACE ( 'NONE', ( #2432 ), #14970, .T. ) ;
#24359=DIRECTION ( 'NONE',  ( -1.000000000000000000, -0.000000000000000000, -0.000000000000000000 ) ) ;
#24367=CIRCLE ( 'NONE', #38793, 0.1000000000000000194 ) ;
#24369=EDGE_CURVE ( 'NONE', #35563, #17308, #19724, .T. ) ;
#24375=VECTOR ( 'NONE', #205, 39.37007874015748143 ) ;
#24381=ORIENTED_EDGE ( 'NONE', *, *, #2355, .T. ) ;
#24392=VERTEX_POINT ( 'NONE', #25243 ) ;
#24403=EDGE_CURVE ( 'NONE', #4635, #4081, #12478, .T. ) ;
#24406=VERTEX_POINT ( 'NONE', #15985 ) ;
#24426=CARTESIAN_POINT ( 'NONE',  ( -0.2746410161513776482, -4.385325017590463226, -0.5985264029706665045 ) ) ;
#24431=VECTOR ( 'NONE', #34359, 39.37007874015748143 ) ;
#24440=AXIS2_PLACEMENT_3D ( 'NONE', #27820, #9281, #40143 ) ;
#24442=CARTESIAN_POINT ( 'NONE',  ( -0.2399999999999999079, -2.139295658456680904, -0.3624034539465684213 ) ) ;
#24443=DIRECTION ( 'NONE',  ( -1.000000000000000000, 0.000000000000000000, 0.000000000000000000 ) ) ;
#24451=LINE ( 'NONE', #28334, #24375 ) ;
#24461=LINE ( 'NONE', #6125, #9313 ) ;
#24486=DIRECTION ( 'NONE',  ( 1.000000000000000000, 0.000000000000000000, 0.000000000000000000 ) ) ;
#24491=EDGE_LOOP ( 'NONE', ( #6812, #23200, #20611, #5813 ) ) ;
#24497=AXIS2_PLACEMENT_3D ( 'NONE', #29428, #1274, #26552 ) ;
#24506=VERTEX_POINT ( 'NONE', #38590 ) ;
#24520=DIRECTION ( 'NONE',  ( 1.000000000000000000, 0.000000000000000000, 0.000000000000000000 ) ) ;
#24549=ORIENTED_EDGE ( 'NONE', *, *, #22230, .F. ) ;
#24567=ORIENTED_EDGE ( 'NONE', *, *, #18557, .F. ) ;
#24570=VECTOR ( 'NONE', #14813, 39.37007874015748143 ) ;
#24593=AXIS2_PLACEMENT_3D ( 'NONE', #40018, #11095, #20360 ) ;
#24618=CARTESIAN_POINT ( 'NONE',  ( -0.2399999999999999079, -2.391283043799508956, -0.6083071156998423046 ) ) ;
#24627=ORIENTED_EDGE ( 'NONE', *, *, #5622, .F. ) ;
#24638=CARTESIAN_POINT ( 'NONE',  ( -0.3000000000000000999, -4.162452804151155483, -0.5855328176471856771 ) ) ;
#24653=DIRECTION ( 'NONE',  ( 0.000000000000000000, 3.414809992080324783E-15, -1.000000000000000000 ) ) ;
#24664=DIRECTION ( 'NONE',  ( 0.4999999999999984457, 0.000000000000000000, -0.8660254037844394848 ) ) ;
#24672=DIRECTION ( 'NONE',  ( 0.4999999999999993894, -0.6415696268731904128, -0.5817116243241110540 ) ) ;
#24677=ORIENTED_EDGE ( 'NONE', *, *, #39715, .T. ) ;
#24678=FACE_OUTER_BOUND ( 'NONE', #15386, .T. ) ;
#24679=PLANE ( 'NONE',  #17810 ) ;
#24685=LINE ( 'NONE', #37215, #22480 ) ;
#24698=ORIENTED_EDGE ( 'NONE', *, *, #11943, .T. ) ;
#24700=ORIENTED_EDGE ( 'NONE', *, *, #37639, .T. ) ;
#24702=LINE ( 'NONE', #9052, #40297 ) ;
#24703=CARTESIAN_POINT ( 'NONE',  ( -0.3000000000000000999, -3.527715956914472706, -0.3920205355121876289 ) ) ;
#24721=AXIS2_PLACEMENT_3D ( 'NONE', #1220, #13722, #26288 ) ;
#24726=DIRECTION ( 'NONE',  ( -1.000000000000000000, 0.000000000000000000, 0.000000000000000000 ) ) ;
#24756=EDGE_LOOP ( 'NONE', ( #28232, #28194, #5551, #40527 ) ) ;
#24792=CARTESIAN_POINT ( 'NONE',  ( -0.3000000000000000999, -2.376910030844113564, -0.7058185084100425666 ) ) ;
#24793=CARTESIAN_POINT ( 'NONE',  ( -0.2746410161513779258, -2.183180860297908144, -0.2991170932241127844 ) ) ;
#24814=VERTEX_POINT ( 'NONE', #6261 ) ;
#24815=DIRECTION ( 'NONE',  ( -1.000000000000000000, -0.000000000000000000, -0.000000000000000000 ) ) ;
#24831=CARTESIAN_POINT ( 'NONE',  ( -0.2746410161513779258, -2.416006048095809877, -1.059240699271965402 ) ) ;
#24904=VERTEX_POINT ( 'NONE', #949 ) ;
#24905=EDGE_LOOP ( 'NONE', ( #8094, #39874, #6222, #12404 ) ) ;
#24920=EDGE_CURVE ( 'NONE', #11635, #1766, #24367, .T. ) ;
#24937=DIRECTION ( 'NONE',  ( 0.000000000000000000, 0.000000000000000000, 1.000000000000000000 ) ) ;
#24940=EDGE_CURVE ( 'NONE', #26277, #19589, #32221, .T. ) ;
#24973=VECTOR ( 'NONE', #22371, 39.37007874015748143 ) ;
#24980=VERTEX_POINT ( 'NONE', #7254 ) ;
#24982=DIRECTION ( 'NONE',  ( -1.000000000000000000, 0.000000000000000000, 0.000000000000000000 ) ) ;
#24983=CONICAL_SURFACE ( 'NONE', #4604, 0.1599999999999999201, 1.047197551196601850 ) ;
#25020=FACE_OUTER_BOUND ( 'NONE', #15933, .T. ) ;
#25028=DIRECTION ( 'NONE',  ( -1.000000000000000000, 0.000000000000000000, 0.000000000000000000 ) ) ;
#25037=VECTOR ( 'NONE', #17460, 39.37007874015748854 ) ;
#25053=CONICAL_SURFACE ( 'NONE', #40132, 0.4615209409081865166, 1.047197551196600740 ) ;
#25068=LINE ( 'NONE', #34527, #7395 ) ;
#25069=CARTESIAN_POINT ( 'NONE',  ( -0.2399999999999999079, -3.811657270145150989, -0.1642545796697100491 ) ) ;
#25095=ORIENTED_EDGE ( 'NONE', *, *, #35438, .F. ) ;
#25110=FACE_OUTER_BOUND ( 'NONE', #37534, .T. ) ;
#25111=CARTESIAN_POINT ( 'NONE',  ( -0.3000000000000000999, -4.233163482269810096, -0.5148221395285308422 ) ) ;
#25113=VECTOR ( 'NONE', #1895, 39.37007874015748143 ) ;
#25121=ADVANCED_FACE ( 'NONE', ( #30714 ), #38159, .F. ) ;
#25127=DIRECTION ( 'NONE',  ( 0.000000000000000000, 0.000000000000000000, 1.000000000000000000 ) ) ;
#25142=EDGE_CURVE ( 'NONE', #9243, #25380, #20866, .T. ) ;
#25147=EDGE_LOOP ( 'NONE', ( #38692, #19396, #26885, #31774 ) ) ;
#25160=LINE ( 'NONE', #9523, #31687 ) ;
#25169=VECTOR ( 'NONE', #22882, 39.37007874015748143 ) ;
#25183=DIRECTION ( 'NONE',  ( 0.000000000000000000, 0.000000000000000000, -1.000000000000000000 ) ) ;
#25191=DIRECTION ( 'NONE',  ( 1.000000000000000000, 0.000000000000000000, 0.000000000000000000 ) ) ;
#25203=VECTOR ( 'NONE', #24089, 39.37007874015748854 ) ;
#25215=CARTESIAN_POINT ( 'NONE',  ( -0.3000000000000000999, -2.761122741982423801, -0.2878817176880067996 ) ) ;
#25219=EDGE_CURVE ( 'NONE', #22886, #10025, #2721, .T. ) ;
#25229=EDGE_CURVE ( 'NONE', #11216, #20247, #10582, .T. ) ;
#25233=CIRCLE ( 'NONE', #14750, 0.1600000000000000588 ) ;
#25243=CARTESIAN_POINT ( 'NONE',  ( -0.3000000000000000999, -2.154189217240303655, -0.3012881438978375903 ) ) ;
#25247=AXIS2_PLACEMENT_3D ( 'NONE', #29740, #32814, #20908 ) ;
#25252=VERTEX_POINT ( 'NONE', #6412 ) ;
#25291=ADVANCED_FACE ( 'NONE', ( #26521 ), #26734, .F. ) ;
#25293=CARTESIAN_POINT ( 'NONE',  ( -0.2746410161513779258, -3.527715956914472706, -0.3920205355121876289 ) ) ;
#25302=ORIENTED_EDGE ( 'NONE', *, *, #7131, .F. ) ;
#25311=ORIENTED_EDGE ( 'NONE', *, *, #20784, .T. ) ;
#25314=ORIENTED_EDGE ( 'NONE', *, *, #16965, .F. ) ;
#25320=VECTOR ( 'NONE', #27399, 39.37007874015748143 ) ;
#25334=VECTOR ( 'NONE', #4916, 39.37007874015748143 ) ;
#25338=DIRECTION ( 'NONE',  ( 0.000000000000000000, 0.000000000000000000, -1.000000000000000000 ) ) ;
#25339=DIRECTION ( 'NONE',  ( -1.000000000000000000, -0.000000000000000000, -0.000000000000000000 ) ) ;
#25355=ORIENTED_EDGE ( 'NONE', *, *, #4505, .F. ) ;
#25364=CIRCLE ( 'NONE', #33902, 0.5515209409081858194 ) ;
#25369=ORIENTED_EDGE ( 'NONE', *, *, #29125, .F. ) ;
#25380=VERTEX_POINT ( 'NONE', #8189 ) ;
#25390=EDGE_CURVE ( 'NONE', #19429, #21211, #1438, .T. ) ;
#25394=AXIS2_PLACEMENT_3D ( 'NONE', #7893, #40401, #14903 ) ;
#25440=CIRCLE ( 'NONE', #39869, 0.1000000000000000194 ) ;
#25472=ORIENTED_EDGE ( 'NONE', *, *, #9934, .F. ) ;
#25476=ORIENTED_EDGE ( 'NONE', *, *, #32500, .T. ) ;
#25493=DIRECTION ( 'NONE',  ( -1.000000000000000000, 0.000000000000000000, 0.000000000000000000 ) ) ;
#25521=EDGE_CURVE ( 'NONE', #12802, #33134, #21379, .T. ) ;
#25524=ORIENTED_EDGE ( 'NONE', *, *, #25793, .T. ) ;
#25537=EDGE_CURVE ( 'NONE', #20247, #16911, #15170, .T. ) ;
#25546=CARTESIAN_POINT ( 'NONE',  ( -0.2399999999999999079, -2.183180860297908144, -0.4312760292030870524 ) ) ;
#25560=VERTEX_POINT ( 'NONE', #18460 ) ;
#25573=ORIENTED_EDGE ( 'NONE', *, *, #3621, .T. ) ;
#25580=EDGE_CURVE ( 'NONE', #19429, #34796, #17807, .T. ) ;
#25583=DIRECTION ( 'NONE',  ( -0.000000000000000000, 0.9246857012436752177, -0.3807313408632030383 ) ) ;
#25597=DIRECTION ( 'NONE',  ( 0.000000000000000000, 0.5365213554527455964, -0.8438867430782097667 ) ) ;
#25601=ORIENTED_EDGE ( 'NONE', *, *, #13558, .T. ) ;
#25608=CARTESIAN_POINT ( 'NONE',  ( -0.2399999999999999079, -3.840189043187996809, -0.1239867222638698224 ) ) ;
#25626=EDGE_CURVE ( 'NONE', #36967, #10025, #19679, .T. ) ;
#25628=DIRECTION ( 'NONE',  ( 0.000000000000000000, 0.000000000000000000, -1.000000000000000000 ) ) ;
#25678=CARTESIAN_POINT ( 'NONE',  ( -0.3000000000000000999, -3.941790907013290823, -0.4709369376873030477 ) ) ;
#25696=DIRECTION ( 'NONE',  ( -0.4999999999999973910, -0.5006794435238203222, 0.7066258520834629575 ) ) ;
#25701=DIRECTION ( 'NONE',  ( -0.000000000000000000, -0.9343694307158671997, 0.3563057211773427713 ) ) ;
#25707=ORIENTED_EDGE ( 'NONE', *, *, #23350, .T. ) ;
#25709=VERTEX_POINT ( 'NONE', #29545 ) ;
#25741=EDGE_CURVE ( 'NONE', #23612, #31054, #14317, .T. ) ;
#25755=CARTESIAN_POINT ( 'NONE',  ( -0.2399999999999999079, -2.341127044584462968, -0.9908042926600856282 ) ) ;
#25760=ORIENTED_EDGE ( 'NONE', *, *, #21085, .F. ) ;
#25767=LINE ( 'NONE', #18403, #119 ) ;
#25788=CONICAL_SURFACE ( 'NONE', #8019, 0.4615209409081865166, 1.047197551196600740 ) ;
#25793=EDGE_CURVE ( 'NONE', #19197, #27945, #10616, .T. ) ;
#25797=DIRECTION ( 'NONE',  ( 0.000000000000000000, 8.195543980992787683E-15, -1.000000000000000000 ) ) ;
#25798=AXIS2_PLACEMENT_3D ( 'NONE', #17095, #4343, #26573 ) ;
#25811=ORIENTED_EDGE ( 'NONE', *, *, #39551, .T. ) ;
#25820=ORIENTED_EDGE ( 'NONE', *, *, #8878, .F. ) ;
#25832=AXIS2_PLACEMENT_3D ( 'NONE', #7208, #35224, #19773 ) ;
#25837=DIRECTION ( 'NONE',  ( 0.000000000000000000, 0.000000000000000000, -1.000000000000000000 ) ) ;
#25849=DIRECTION ( 'NONE',  ( 1.000000000000000000, 0.000000000000000000, 0.000000000000000000 ) ) ;
#25854=AXIS2_PLACEMENT_3D ( 'NONE', #33462, #33892, #5269 ) ;
#25868=DIRECTION ( 'NONE',  ( 0.000000000000000000, 0.000000000000000000, -1.000000000000000000 ) ) ;
#25870=CARTESIAN_POINT ( 'NONE',  ( -0.2746410161513779258, -2.761122741982423801, -0.2878817176880067996 ) ) ;
#25902=DIRECTION ( 'NONE',  ( 1.000000000000000000, 0.000000000000000000, 0.000000000000000000 ) ) ;
#25904=EDGE_CURVE ( 'NONE', #8729, #354, #33437, .T. ) ;
#25907=DIRECTION ( 'NONE',  ( -1.000000000000000000, -0.000000000000000000, -0.000000000000000000 ) ) ;
#25909=LINE ( 'NONE', #32240, #33665 ) ;
#25941=VERTEX_POINT ( 'NONE', #11833 ) ;
#25945=CARTESIAN_POINT ( 'NONE',  ( -0.2746410161513779258, -3.970782550070895311, -0.6634248229925526763 ) ) ;
#25960=DIRECTION ( 'NONE',  ( -0.000000000000000000, 0.5781348229923758408, -0.8159412518334724362 ) ) ;
#26001=AXIS2_PLACEMENT_3D ( 'NONE', #2584, #24815, #146 ) ;
#26016=ORIENTED_EDGE ( 'NONE', *, *, #33563, .T. ) ;
#26047=CONICAL_SURFACE ( 'NONE', #24721, 0.1600000000000004752, 1.047197551196598519 ) ;
#26058=ORIENTED_EDGE ( 'NONE', *, *, #13374, .T. ) ;
#26061=CARTESIAN_POINT ( 'NONE',  ( -0.2399999999999999079, -2.183180860297908144, -0.4937760292030871079 ) ) ;
#26065=CARTESIAN_POINT ( 'NONE',  ( -0.2399999999999999079, -3.384162466027138105, -0.4389494074304161608 ) ) ;
#26066=DIRECTION ( 'NONE',  ( -1.000000000000000000, -0.000000000000000000, -0.000000000000000000 ) ) ;
#26076=DIRECTION ( 'NONE',  ( 1.000000000000000000, 0.000000000000000000, 0.000000000000000000 ) ) ;
#26109=CARTESIAN_POINT ( 'NONE',  ( -0.2746410161513779258, -2.809880844172510272, -0.2480969101616946337 ) ) ;
#26125=EDGE_LOOP ( 'NONE', ( #2168, #9443, #36067, #13945 ) ) ;
#26127=VERTEX_POINT ( 'NONE', #37442 ) ;
#26135=ORIENTED_EDGE ( 'NONE', *, *, #21482, .T. ) ;
#26141=EDGE_CURVE ( 'NONE', #20593, #13608, #21831, .T. ) ;
#26154=CARTESIAN_POINT ( 'NONE',  ( -0.2746410161513782033, -2.183180860297908144, -0.4937760292030871079 ) ) ;
#26166=CARTESIAN_POINT ( 'NONE',  ( -0.2399999999999999079, -3.253295730098268113, -0.6063490597057096254 ) ) ;
#26168=CARTESIAN_POINT ( 'NONE',  ( -0.2399999999999999079, -2.845511416290244622, -0.3415338532332813926 ) ) ;
#26195=( NAMED_UNIT ( * ) PLANE_ANGLE_UNIT ( ) SI_UNIT ( $, .RADIAN. ) );
#26209=CARTESIAN_POINT ( 'NONE',  ( -0.3000000000000000999, -2.377058624452622393, -0.8919706583825134372 ) ) ;
#26272=ADVANCED_FACE ( 'NONE', ( #32090 ), #4307, .F. ) ;
#26277=VERTEX_POINT ( 'NONE', #3897 ) ;
#26288=DIRECTION ( 'NONE',  ( 0.000000000000000000, 0.000000000000000000, -1.000000000000000000 ) ) ;
#26289=DIRECTION ( 'NONE',  ( 0.000000000000000000, -0.8159412518334724362, -0.5781348229923761739 ) ) ;
#26304=ORIENTED_EDGE ( 'NONE', *, *, #13288, .F. ) ;
#26308=VERTEX_POINT ( 'NONE', #14625 ) ;
#26327=DIRECTION ( 'NONE',  ( -0.4379975771764339498, -0.8989761522908011893, 0.000000000000000000 ) ) ;
#26335=CARTESIAN_POINT ( 'NONE',  ( -0.3000000000000000999, -2.323257895298838971, -0.7902071827178637209 ) ) ;
#26337=DIRECTION ( 'NONE',  ( 1.000000000000000000, -0.000000000000000000, -0.000000000000000000 ) ) ;
#26342=LINE ( 'NONE', #16887, #30391 ) ;
#26367=EDGE_CURVE ( 'NONE', #12802, #25709, #36033, .T. ) ;
#26383=DIRECTION ( 'NONE',  ( 0.000000000000000000, 0.000000000000000000, 1.000000000000000000 ) ) ;
#26384=AXIS2_PLACEMENT_3D ( 'NONE', #4545, #11141, #20617 ) ;
#26410=DIRECTION ( 'NONE',  ( -1.000000000000000000, -0.000000000000000000, -0.000000000000000000 ) ) ;
#26449=DIRECTION ( 'NONE',  ( 1.000000000000000000, -0.000000000000000000, -0.000000000000000000 ) ) ;
#26453=CARTESIAN_POINT ( 'NONE',  ( -0.3000000000000000999, -3.253295730098268113, -0.6063490597057096254 ) ) ;
#26466=DIRECTION ( 'NONE',  ( 0.000000000000000000, 0.000000000000000000, 1.000000000000000000 ) ) ;
#26468=DIRECTION ( 'NONE',  ( 0.000000000000000000, -0.8159412518334721032, -0.5781348229923762849 ) ) ;
#26471=CIRCLE ( 'NONE', #37002, 0.1000000000000000194 ) ;
#26474=DIRECTION ( 'NONE',  ( -1.000000000000000000, -0.000000000000000000, -0.000000000000000000 ) ) ;
#26475=VERTEX_POINT ( 'NONE', #30476 ) ;
#26491=FACE_OUTER_BOUND ( 'NONE', #6410, .T. ) ;
#26516=AXIS2_PLACEMENT_3D ( 'NONE', #39159, #26410, #29295 ) ;
#26521=FACE_OUTER_BOUND ( 'NONE', #7407, .T. ) ;
#26532=EDGE_CURVE ( 'NONE', #20383, #34142, #11939, .T. ) ;
#26540=DIRECTION ( 'NONE',  ( 0.000000000000000000, -0.8438867430782092116, -0.5365213554527465956 ) ) ;
#26543=EDGE_CURVE ( 'NONE', #11891, #12319, #29056, .T. ) ;
#26552=DIRECTION ( 'NONE',  ( 0.000000000000000000, 0.000000000000000000, -1.000000000000000000 ) ) ;
#26558=CARTESIAN_POINT ( 'NONE',  ( -0.2399999999999999079, -3.739689364820627748, -0.3461216533844236887 ) ) ;
#26565=CIRCLE ( 'NONE', #37062, 0.1000000000000000194 ) ;
#26573=DIRECTION ( 'NONE',  ( 0.000000000000000000, 0.000000000000000000, 1.000000000000000000 ) ) ;
#26581=CARTESIAN_POINT ( 'NONE',  ( -0.2746410161513770931, -2.853330612949663170, -0.6088139570729240724 ) ) ;
#26588=ADVANCED_FACE ( 'NONE', ( #18748 ), #33972, .F. ) ;
#26603=AXIS2_PLACEMENT_3D ( 'NONE', #16237, #10047, #6538 ) ;
#26613=ADVANCED_FACE ( 'NONE', ( #35785 ), #485, .F. ) ;
#26617=AXIS2_PLACEMENT_3D ( 'NONE', #29930, #36276, #21677 ) ;
#26629=VERTEX_POINT ( 'NONE', #28810 ) ;
#26634=ORIENTED_EDGE ( 'NONE', *, *, #4995, .F. ) ;
#26638=CARTESIAN_POINT ( 'NONE',  ( -0.3000000000000000999, -3.811657270145150989, -0.1642545796697100491 ) ) ;
#26641=ORIENTED_EDGE ( 'NONE', *, *, #3126, .F. ) ;
#26655=ADVANCED_FACE ( 'NONE', ( #10087 ), #22659, .F. ) ;
#26673=AXIS2_PLACEMENT_3D ( 'NONE', #21074, #33599, #17974 ) ;
#26697=CARTESIAN_POINT ( 'NONE',  ( -0.3000000000000000999, -2.423474325126674156, -0.5576739111151495232 ) ) ;
#26699=EDGE_LOOP ( 'NONE', ( #34188, #18267, #22948, #1642 ) ) ;
#26705=LINE ( 'NONE', #7548, #37821 ) ;
#26723=VERTEX_POINT ( 'NONE', #1265 ) ;
#26734=CYLINDRICAL_SURFACE ( 'NONE', #9260, 0.1000000000000000056 ) ;
#26743=CARTESIAN_POINT ( 'NONE',  ( -0.2399999999999999079, -3.941790907013290823, -0.4709369376873030477 ) ) ;
#26755=FACE_OUTER_BOUND ( 'NONE', #10325, .T. ) ;
#26760=CARTESIAN_POINT ( 'NONE',  ( -0.3000000000000000999, -1.906460133321048911, -0.3231213194042101278 ) ) ;
#26762=ORIENTED_EDGE ( 'NONE', *, *, #950, .T. ) ;
#26771=ORIENTED_EDGE ( 'NONE', *, *, #30275, .T. ) ;
#26778=EDGE_CURVE ( 'NONE', #27000, #18456, #9999, .T. ) ;
#26802=DIRECTION ( 'NONE',  ( -1.000000000000000000, -0.000000000000000000, -0.000000000000000000 ) ) ;
#26805=SHAPE_REPRESENTATION_RELATIONSHIP ( 'NONE' , 'NONE' ,  #21742, #7338 ) ;
#26817=EDGE_CURVE ( 'NONE', #15882, #33666, #20364, .T. ) ;
#26822=EDGE_CURVE ( 'NONE', #35653, #14911, #33100, .T. ) ;
#26826=EDGE_LOOP ( 'NONE', ( #6613, #35759 ) ) ;
#26855=CARTESIAN_POINT ( 'NONE',  ( -0.2399999999999999079, -2.183180860297908144, -0.4312760292030870524 ) ) ;
#26856=ORIENTED_EDGE ( 'NONE', *, *, #31928, .T. ) ;
#26858=CYLINDRICAL_SURFACE ( 'NONE', #18586, 0.6115209409081865388 ) ;
#26859=DIRECTION ( 'NONE',  ( 0.000000000000000000, 0.000000000000000000, 1.000000000000000000 ) ) ;
#26885=ORIENTED_EDGE ( 'NONE', *, *, #18050, .F. ) ;
#26903=CARTESIAN_POINT ( 'NONE',  ( -0.2399999999999999079, -3.156018320128275878, -0.4841849112664152743 ) ) ;
#26912=ORIENTED_EDGE ( 'NONE', *, *, #661, .F. ) ;
#26935=DIRECTION ( 'NONE',  ( 0.000000000000000000, 0.000000000000000000, -1.000000000000000000 ) ) ;
#26936=ADVANCED_FACE ( 'NONE', ( #21783 ), #11898, .F. ) ;
#26943=CARTESIAN_POINT ( 'NONE',  ( -0.2399999999999999079, -3.941790907013290823, -0.4709369376873030477 ) ) ;
#26983=EDGE_CURVE ( 'NONE', #4836, #36854, #24461, .T. ) ;
#26987=CONICAL_SURFACE ( 'NONE', #16473, 0.1346589359789736318, 1.047197551196598742 ) ;
#27000=VERTEX_POINT ( 'NONE', #21171 ) ;
#27001=CARTESIAN_POINT ( 'NONE',  ( -0.3000000000000000999, -2.183180860297908144, -0.4937760292030871079 ) ) ;
#27004=EDGE_LOOP ( 'NONE', ( #29131, #14818, #11942, #30145, #35974, #23367, #26016, #25524, #26762, #4842, #8066, #12233, #12303 ) ) ;
#27008=VECTOR ( 'NONE', #24664, 39.37007874015748854 ) ;
#27025=LINE ( 'NONE', #8299, #33706 ) ;
#27032=ORIENTED_EDGE ( 'NONE', *, *, #35885, .F. ) ;
#27047=AXIS2_PLACEMENT_3D ( 'NONE', #29349, #1977, #1191 ) ;
#27051=CARTESIAN_POINT ( 'NONE',  ( -0.2399999999999999079, -2.477126460671948749, -0.4732852368073287574 ) ) ;
#27067=VECTOR ( 'NONE', #20779, 39.37007874015748143 ) ;
#27118=ORIENTED_EDGE ( 'NONE', *, *, #38128, .F. ) ;
#27126=ORIENTED_EDGE ( 'NONE', *, *, #30843, .T. ) ;
#27128=VERTEX_POINT ( 'NONE', #7126 ) ;
#27147=LINE ( 'NONE', #11296, #14129 ) ;
#27157=APPLICATION_CONTEXT ( 'configuration controlled 3d designs of mechanical parts and assemblies' ) ;
#27162=AXIS2_PLACEMENT_3D ( 'NONE', #29463, #1307, #26383 ) ;
#27163=CARTESIAN_POINT ( 'NONE',  ( -0.2399999999999999079, -2.511040369707300268, -0.4948468226404901804 ) ) ;
#27165=EDGE_LOOP ( 'NONE', ( #32569, #14248, #7399, #8487 ) ) ;
#27167=ORIENTED_EDGE ( 'NONE', *, *, #30268, .F. ) ;
#27168=AXIS2_PLACEMENT_3D ( 'NONE', #30654, #2475, #17879 ) ;
#27172=FACE_OUTER_BOUND ( 'NONE', #30452, .T. ) ;
#27176=VECTOR ( 'NONE', #33889, 39.37007874015748143 ) ;
#27215=DIRECTION ( 'NONE',  ( -1.000000000000000000, -0.000000000000000000, -0.000000000000000000 ) ) ;
#27226=VERTEX_POINT ( 'NONE', #29560 ) ;
#27229=AXIS2_PLACEMENT_3D ( 'NONE', #13045, #10160, #25597 ) ;
#27253=EDGE_CURVE ( 'NONE', #40377, #34047, #10853, .T. ) ;
#27274=DIRECTION ( 'NONE',  ( 0.8660254037844402619, -0.1903656704316006587, -0.4623428506218351663 ) ) ;
#27276=ORIENTED_EDGE ( 'NONE', *, *, #25904, .F. ) ;
#27283=EDGE_CURVE ( 'NONE', #38708, #11216, #20728, .T. ) ;
#27288=DIRECTION ( 'NONE',  ( 0.000000000000000000, 0.000000000000000000, -1.000000000000000000 ) ) ;
#27290=VECTOR ( 'NONE', #37918, 39.37007874015748143 ) ;
#27307=LINE ( 'NONE', #21121, #6209 ) ;
#27308=ADVANCED_FACE ( 'NONE', ( #11847 ), #25788, .F. ) ;
#27353=ORIENTED_EDGE ( 'NONE', *, *, #11992, .F. ) ;
#27363=EDGE_CURVE ( 'NONE', #1766, #38965, #37160, .T. ) ;
#27373=CARTESIAN_POINT ( 'NONE',  ( -0.2399999999999999079, -2.945416957892569521, -0.4639726661791638840 ) ) ;
#27376=CARTESIAN_POINT ( 'NONE',  ( -0.2746410161513776482, -3.840189043187996809, -0.1239867222638698224 ) ) ;
#27378=VECTOR ( 'NONE', #24672, 39.37007874015748854 ) ;
#27383=ORIENTED_EDGE ( 'NONE', *, *, #2671, .F. ) ;
#27392=VECTOR ( 'NONE', #35939, 39.37007874015748143 ) ;
#27399=DIRECTION ( 'NONE',  ( 1.000000000000000000, 0.000000000000000000, 0.000000000000000000 ) ) ;
#27434=ORIENTED_EDGE ( 'NONE', *, *, #35060, .T. ) ;
#27449=ORIENTED_EDGE ( 'NONE', *, *, #25904, .T. ) ;
#27450=VERTEX_POINT ( 'NONE', #34672 ) ;
#27451=DIRECTION ( 'NONE',  ( 0.000000000000000000, 0.000000000000000000, -1.000000000000000000 ) ) ;
#27484=ORIENTED_EDGE ( 'NONE', *, *, #10734, .T. ) ;
#27493=CARTESIAN_POINT ( 'NONE',  ( -0.3000000000000000999, -2.477126460671948749, -0.4732852368073287574 ) ) ;
#27502=EDGE_CURVE ( 'NONE', #9331, #11583, #1509, .T. ) ;
#27520=ORIENTED_EDGE ( 'NONE', *, *, #35305, .T. ) ;
#27534=ORIENTED_EDGE ( 'NONE', *, *, #36555, .T. ) ;
#27540=DIRECTION ( 'NONE',  ( 0.000000000000000000, -0.7071067811865465735, -0.7071067811865484609 ) ) ;
#27585=VERTEX_POINT ( 'NONE', #16923 ) ;
#27595=DIRECTION ( 'NONE',  ( 0.8660254037844378194, -0.2682606777263741304, 0.4219433715391058826 ) ) ;
#27597=CARTESIAN_POINT ( 'NONE',  ( -0.3000000000000000999, -3.647187793141847045, -0.4766722536777797115 ) ) ;
#27599=PLANE ( 'NONE',  #15364 ) ;
#27604=AXIS2_PLACEMENT_3D ( 'NONE', #24289, #15022, #11925 ) ;
#27618=ADVANCED_FACE ( 'NONE', ( #4750, #20833, #8457, #36837, #21021, #11149 ), #5576, .T. ) ;
#27624=ORIENTED_EDGE ( 'NONE', *, *, #35078, .T. ) ;
#27642=CARTESIAN_POINT ( 'NONE',  ( -0.2399999999999999079, -2.292669950144801572, -0.8383185228372386222 ) ) ;
#27645=DIRECTION ( 'NONE',  ( 0.000000000000000000, 0.000000000000000000, 1.000000000000000000 ) ) ;
#27679=ORIENTED_EDGE ( 'NONE', *, *, #40406, .T. ) ;
#27707=CARTESIAN_POINT ( 'NONE',  ( -0.3000000000000000999, -2.376910030844113564, -0.7058185084100425666 ) ) ;
#27717=AXIS2_PLACEMENT_3D ( 'NONE', #26581, #19780, #10122 ) ;
#27739=EDGE_CURVE ( 'NONE', #27741, #27226, #12002, .T. ) ;
#27741=VERTEX_POINT ( 'NONE', #15049 ) ;
#27764=DIRECTION ( 'NONE',  ( 0.000000000000000000, 0.000000000000000000, -1.000000000000000000 ) ) ;
#27769=ORIENTED_EDGE ( 'NONE', *, *, #15694, .F. ) ;
#27777=LINE ( 'NONE', #39917, #34324 ) ;
#27783=CARTESIAN_POINT ( 'NONE',  ( -0.2746410161513779258, -4.056386786973173564, -0.6915988348251679296 ) ) ;
#27791=ORIENTED_EDGE ( 'NONE', *, *, #6908, .T. ) ;
#27806=LINE ( 'NONE', #15464, #21408 ) ;
#27815=AXIS2_PLACEMENT_3D ( 'NONE', #23833, #36354, #2017 ) ;
#27819=AXIS2_PLACEMENT_3D ( 'NONE', #8920, #2961, #8315 ) ;
#27820=CARTESIAN_POINT ( 'NONE',  ( -0.2399999999999999079, -2.323257895298838971, -0.7902071827178637209 ) ) ;
#27821=VERTEX_POINT ( 'NONE', #18752 ) ;
#27822=CARTESIAN_POINT ( 'NONE',  ( -0.3000000000000000999, -3.291368864184587739, -0.6988176298300774469 ) ) ;
#27837=ORIENTED_EDGE ( 'NONE', *, *, #16782, .F. ) ;
#27850=AXIS2_PLACEMENT_3D ( 'NONE', #3813, #22169, #12888 ) ;
#27853=CIRCLE ( 'NONE', #35068, 0.1600000000000007527 ) ;
#27898=CARTESIAN_POINT ( 'NONE',  ( -0.2399999999999999079, -2.183180860297908144, -0.5562760292030870524 ) ) ;
#27900=DIRECTION ( 'NONE',  ( -1.000000000000000000, -0.000000000000000000, -0.000000000000000000 ) ) ;
#27919=CARTESIAN_POINT ( 'NONE',  ( -0.2399999999999999079, -2.461298705151934829, -0.7594706439553173816 ) ) ;
#27942=VECTOR ( 'NONE', #3018, 39.37007874015748854 ) ;
#27945=VERTEX_POINT ( 'NONE', #3514 ) ;
#27962=CARTESIAN_POINT ( 'NONE',  ( -0.2399999999999999079, -3.961846414800720861, -0.6040940090217902236 ) ) ;
#27971=AXIS2_PLACEMENT_3D ( 'NONE', #20371, #4707, #1670 ) ;
#27972=DIRECTION ( 'NONE',  ( 0.000000000000000000, 6.829619984160661399E-15, -1.000000000000000000 ) ) ;
#27974=DIRECTION ( 'NONE',  ( 0.4999999999999955591, 0.000000000000000000, -0.8660254037844411501 ) ) ;
#27977=VERTEX_POINT ( 'NONE', #487 ) ;
#27988=ORIENTED_EDGE ( 'NONE', *, *, #30340, .F. ) ;
#28008=DIRECTION ( 'NONE',  ( 0.000000000000000000, 0.000000000000000000, -1.000000000000000000 ) ) ;
#28026=DIRECTION ( 'NONE',  ( 0.4261641068392729714, 0.9046458721742364206, 0.000000000000000000 ) ) ;
#28029=EDGE_CURVE ( 'NONE', #4635, #35563, #16274, .T. ) ;
#28033=LINE ( 'NONE', #30896, #164 ) ;
#28035=CARTESIAN_POINT ( 'NONE',  ( -0.2399999999999999079, -4.289222312108804225, -0.5708809693675255259 ) ) ;
#28038=CARTESIAN_POINT ( 'NONE',  ( -0.3000000000000000999, -3.941790907013290823, -0.4709369376873030477 ) ) ;
#28042=ORIENTED_EDGE ( 'NONE', *, *, #17915, .F. ) ;
#28081=CARTESIAN_POINT ( 'NONE',  ( -0.2399999999999999079, -4.218511633990150500, -0.6415916474861803609 ) ) ;
#28104=DIRECTION ( 'NONE',  ( 0.4747798520620566398, 0.000000000000000000, 0.8801045915548512122 ) ) ;
#28109=CARTESIAN_POINT ( 'NONE',  ( -0.2746410161513782033, -2.183180860297908144, -0.4937760292030871079 ) ) ;
#28112=CARTESIAN_POINT ( 'NONE',  ( -0.2399999999999999079, -4.250025578259899461, -0.8852376261118949374 ) ) ;
#28122=DIRECTION ( 'NONE',  ( 1.000000000000000000, 0.000000000000000000, 0.000000000000000000 ) ) ;
#28123=ORIENTED_EDGE ( 'NONE', *, *, #32364, .F. ) ;
#28127=CARTESIAN_POINT ( 'NONE',  ( -0.2746410161513779258, -2.761122741982423801, -0.2878817176880067996 ) ) ;
#28138=ORIENTED_EDGE ( 'NONE', *, *, #1522, .T. ) ;
#28140=ORIENTED_EDGE ( 'NONE', *, *, #7614, .F. ) ;
#28141=ADVANCED_FACE ( 'NONE', ( #36185 ), #23210, .T. ) ;
#28154=ORIENTED_EDGE ( 'NONE', *, *, #31822, .F. ) ;
#28168=LINE ( 'NONE', #3677, #7505 ) ;
#28173=FACE_OUTER_BOUND ( 'NONE', #13263, .T. ) ;
#28194=ORIENTED_EDGE ( 'NONE', *, *, #38083, .F. ) ;
#28215=CARTESIAN_POINT ( 'NONE',  ( -0.2399999999999999079, -2.183180860297908144, -0.3591170932241134484 ) ) ;
#28228=CARTESIAN_POINT ( 'NONE',  ( -0.2746410161513776482, -3.849534981189179028, -0.1910928155360645808 ) ) ;
#28229=DIRECTION ( 'NONE',  ( -1.000000000000000000, -0.000000000000000000, -0.000000000000000000 ) ) ;
#28231=CARTESIAN_POINT ( 'NONE',  ( -0.2399999999999999079, -2.154189217240303655, -0.3012881438978375903 ) ) ;
#28232=ORIENTED_EDGE ( 'NONE', *, *, #40595, .F. ) ;
#28240=ORIENTED_EDGE ( 'NONE', *, *, #15256, .F. ) ;
#28247=LINE ( 'NONE', #15905, #466 ) ;
#28269=AXIS2_PLACEMENT_3D ( 'NONE', #1326, #35257, #23341 ) ;
#28276=ORIENTED_EDGE ( 'NONE', *, *, #7983, .F. ) ;
#28334=CARTESIAN_POINT ( 'NONE',  ( -0.2399999999999999079, -3.730063144961804245, -0.1064410973704724706 ) ) ;
#28336=CARTESIAN_POINT ( 'NONE',  ( -0.2399999999999999079, -3.701811653776600597, -0.3192834175180690459 ) ) ;
#28340=ORIENTED_EDGE ( 'NONE', *, *, #40559, .F. ) ;
#28347=FACE_OUTER_BOUND ( 'NONE', #31871, .T. ) ;
#28356=EDGE_CURVE ( 'NONE', #9095, #21137, #6531, .T. ) ;
#28363=EDGE_CURVE ( 'NONE', #6766, #8015, #25068, .T. ) ;
#28371=AXIS2_PLACEMENT_3D ( 'NONE', #7510, #26066, #1370 ) ;
#28382=VERTEX_POINT ( 'NONE', #21592 ) ;
#28386=ORIENTED_EDGE ( 'NONE', *, *, #17205, .T. ) ;
#28390=FACE_OUTER_BOUND ( 'NONE', #4232, .T. ) ;
#28393=VECTOR ( 'NONE', #33255, 39.37007874015748143 ) ;
#28405=CARTESIAN_POINT ( 'NONE',  ( -0.2746410161513779258, -2.183180860297908144, -0.4937760292030871079 ) ) ;
#28410=DIRECTION ( 'NONE',  ( -0.000000000000000000, -0.9343694307158671997, 0.3563057211773426602 ) ) ;
#28428=ORIENTED_EDGE ( 'NONE', *, *, #28363, .T. ) ;
#28431=ORIENTED_EDGE ( 'NONE', *, *, #17546, .F. ) ;
#28446=LINE ( 'NONE', #22494, #16101 ) ;
#28453=CIRCLE ( 'NONE', #29781, 0.1600000000000005584 ) ;
#28455=PRODUCT_CONTEXT ( 'NONE', #27157, 'mechanical' ) ;
#28465=AXIS2_PLACEMENT_3D ( 'NONE', #19264, #38167, #3619 ) ;
#28467=VERTEX_POINT ( 'NONE', #4266 ) ;
#28470=VERTEX_POINT ( 'NONE', #13119 ) ;
#28478=LINE ( 'NONE', #6654, #35334 ) ;
#28481=LINE ( 'NONE', #355, #35681 ) ;
#28496=DIRECTION ( 'NONE',  ( 0.4999999999999940603, 0.7308273574226435976, 0.4646411234949414659 ) ) ;
#28507=VECTOR ( 'NONE', #22073, 39.37007874015748854 ) ;
#28512=FACE_OUTER_BOUND ( 'NONE', #12857, .T. ) ;
#28515=DIRECTION ( 'NONE',  ( 0.000000000000000000, -0.5365213554527478168, 0.8438867430782083234 ) ) ;
#28524=CARTESIAN_POINT ( 'NONE',  ( -0.2399999999999999079, -1.874946189051298617, -0.07947534077849525980 ) ) ;
#28533=VECTOR ( 'NONE', #29495, 39.37007874015748143 ) ;
#28543=AXIS2_PLACEMENT_3D ( 'NONE', #12906, #34898, #12688 ) ;
#28570=CIRCLE ( 'NONE', #33820, 0.1600000000000004752 ) ;
#28573=LINE ( 'NONE', #16417, #32380 ) ;
#28601=CARTESIAN_POINT ( 'NONE',  ( -0.3000000000000000999, -1.730153431576819001, -0.08301574631829751472 ) ) ;
#28605=LINE ( 'NONE', #9250, #1457 ) ;
#28632=VECTOR ( 'NONE', #13432, 39.37007874015748854 ) ;
#28634=ORIENTED_EDGE ( 'NONE', *, *, #177, .F. ) ;
#28636=ORIENTED_EDGE ( 'NONE', *, *, #29512, .T. ) ;
#28645=ORIENTED_EDGE ( 'NONE', *, *, #33707, .T. ) ;
#28680=LINE ( 'NONE', #547, #17755 ) ;
#28687=ORIENTED_EDGE ( 'NONE', *, *, #21203, .F. ) ;
#28693=CARTESIAN_POINT ( 'NONE',  ( -0.2399999999999999079, -3.941790907013290823, -0.3362780017083292772 ) ) ;
#28698=VERTEX_POINT ( 'NONE', #37360 ) ;
#28709=ORIENTED_EDGE ( 'NONE', *, *, #17073, .T. ) ;
#28716=CARTESIAN_POINT ( 'NONE',  ( -0.2399999999999999079, -3.970782550070895311, -0.6634248229925526763 ) ) ;
#28719=VECTOR ( 'NONE', #16736, 39.37007874015748854 ) ;
#28740=CARTESIAN_POINT ( 'NONE',  ( -0.3000000000000000999, -3.941790907013290823, -0.4709369376873030477 ) ) ;
#28746=ORIENTED_EDGE ( 'NONE', *, *, #6247, .F. ) ;
#28753=EDGE_LOOP ( 'NONE', ( #38833, #2079, #4038, #35499 ) ) ;
#28754=LINE ( 'NONE', #32222, #31983 ) ;
#28771=CARTESIAN_POINT ( 'NONE',  ( -0.2399999999999999079, -3.609310082097819894, -0.4498340178114252352 ) ) ;
#28774=FACE_OUTER_BOUND ( 'NONE', #13607, .T. ) ;
#28777=ADVANCED_FACE ( 'NONE', ( #35695 ), #38761, .F. ) ;
#28784=ORIENTED_EDGE ( 'NONE', *, *, #33303, .T. ) ;
#28797=DIRECTION ( 'NONE',  ( 0.000000000000000000, 0.000000000000000000, -1.000000000000000000 ) ) ;
#28803=EDGE_LOOP ( 'NONE', ( #3177, #11554, #10732, #19089 ) ) ;
#28810=CARTESIAN_POINT ( 'NONE',  ( -0.3000000000000000999, -3.237612445311622622, -0.5419983935656527141 ) ) ;
#28818=DIRECTION ( 'NONE',  ( -1.000000000000000000, -0.000000000000000000, -0.000000000000000000 ) ) ;
#28831=ORIENTED_EDGE ( 'NONE', *, *, #32605, .T. ) ;
#28842=DIRECTION ( 'NONE',  ( 1.000000000000000000, -0.000000000000000000, -0.000000000000000000 ) ) ;
#28845=ORIENTED_EDGE ( 'NONE', *, *, #33417, .F. ) ;
#28860=CARTESIAN_POINT ( 'NONE',  ( -0.2746410161513779258, -2.477126460671948749, -0.4732852368073287574 ) ) ;
#28901=DIRECTION ( 'NONE',  ( 0.5000000000000009992, -0.7308273574226402669, -0.4646411234949391900 ) ) ;
#28913=ORIENTED_EDGE ( 'NONE', *, *, #27253, .T. ) ;
#28914=DIRECTION ( 'NONE',  ( -0.000000000000000000, -0.5365213554527455964, 0.8438867430782097667 ) ) ;
#28923=CARTESIAN_POINT ( 'NONE',  ( -0.3000000000000000999, -2.878813263491020180, -0.3823467908819087602 ) ) ;
#28932=ORIENTED_EDGE ( 'NONE', *, *, #17255, .T. ) ;
#28968=VERTEX_POINT ( 'NONE', #35427 ) ;
#28979=DIRECTION ( 'NONE',  ( 1.000000000000000000, -0.000000000000000000, -0.000000000000000000 ) ) ;
#29001=CARTESIAN_POINT ( 'NONE',  ( -0.2399999999999999079, -2.289343986263487896, -0.7686455968847020204 ) ) ;
#29003=AXIS2_PLACEMENT_3D ( 'NONE', #13761, #32276, #26327 ) ;
#29011=AXIS2_PLACEMENT_3D ( 'NONE', #14647, #27215, #33559 ) ;
#29015=DIRECTION ( 'NONE',  ( 1.000000000000000000, -0.000000000000000000, -0.000000000000000000 ) ) ;
#29018=LINE ( 'NONE', #25546, #40544 ) ;
#29020=ADVANCED_FACE ( 'NONE', ( #32540 ), #4358, .T. ) ;
#29021=LINE ( 'NONE', #689, #6679 ) ;
#29030=ORIENTED_EDGE ( 'NONE', *, *, #18803, .T. ) ;
#29035=AXIS2_PLACEMENT_3D ( 'NONE', #37342, #7984, #17467 ) ;
#29040=AXIS2_PLACEMENT_3D ( 'NONE', #12627, #25191, #37735 ) ;
#29056=CIRCLE ( 'NONE', #11320, 0.1946589359789743512 ) ;
#29063=AXIS2_PLACEMENT_3D ( 'NONE', #1039, #29384, #23439 ) ;
#29065=AXIS2_PLACEMENT_3D ( 'NONE', #38089, #3538, #38287 ) ;
#29071=DIRECTION ( 'NONE',  ( 0.000000000000000000, -0.9246857012436752177, 0.3807313408632033713 ) ) ;
#29082=VERTEX_POINT ( 'NONE', #26209 ) ;
#29087=ORIENTED_EDGE ( 'NONE', *, *, #11241, .F. ) ;
#29097=EDGE_CURVE ( 'NONE', #34796, #12108, #33185, .T. ) ;
#29099=ORIENTED_EDGE ( 'NONE', *, *, #10734, .F. ) ;
#29101=VECTOR ( 'NONE', #21159, 39.37007874015748143 ) ;
#29108=FACE_OUTER_BOUND ( 'NONE', #33812, .T. ) ;
#29125=EDGE_CURVE ( 'NONE', #18610, #35757, #32969, .T. ) ;
#29129=EDGE_CURVE ( 'NONE', #25252, #31920, #21263, .T. ) ;
#29131=ORIENTED_EDGE ( 'NONE', *, *, #23821, .T. ) ;
#29147=DIRECTION ( 'NONE',  ( 0.000000000000000000, 0.000000000000000000, 1.000000000000000000 ) ) ;
#29151=ADVANCED_FACE ( 'NONE', ( #1928 ), #17347, .F. ) ;
#29156=DIRECTION ( 'NONE',  ( 1.000000000000000000, 0.000000000000000000, 0.000000000000000000 ) ) ;
#29161=FACE_OUTER_BOUND ( 'NONE', #10116, .T. ) ;
#29167=CIRCLE ( 'NONE', #6801, 0.1000000000000000194 ) ;
#29175=CYLINDRICAL_SURFACE ( 'NONE', #37669, 0.1000000000000000194 ) ;
#29188=ORIENTED_EDGE ( 'NONE', *, *, #36575, .F. ) ;
#29214=AXIS2_PLACEMENT_3D ( 'NONE', #4574, #14265, #39546 ) ;
#29219=AXIS2_PLACEMENT_3D ( 'NONE', #26943, #23872, #30217 ) ;
#29238=VECTOR ( 'NONE', #5337, 39.37007874015748854 ) ;
#29257=AXIS2_PLACEMENT_3D ( 'NONE', #5736, #9036, #34120 ) ;
#29261=FACE_OUTER_BOUND ( 'NONE', #37701, .T. ) ;
#29275=VECTOR ( 'NONE', #6780, 39.37007874015747433 ) ;
#29276=EDGE_CURVE ( 'NONE', #13608, #15882, #24702, .T. ) ;
#29278=CIRCLE ( 'NONE', #34526, 0.1000000000000000194 ) ;
#29286=CIRCLE ( 'NONE', #29257, 0.1600000000000016409 ) ;
#29295=DIRECTION ( 'NONE',  ( 0.000000000000000000, 0.000000000000000000, 1.000000000000000000 ) ) ;
#29332=CIRCLE ( 'NONE', #39841, 0.1600000000000006140 ) ;
#29343=DIRECTION ( 'NONE',  ( 0.000000000000000000, 0.000000000000000000, -1.000000000000000000 ) ) ;
#29344=AXIS2_PLACEMENT_3D ( 'NONE', #13225, #13439, #37927 ) ;
#29349=CARTESIAN_POINT ( 'NONE',  ( -0.3000000000000000999, -2.183180860297908144, -0.4937760292030871079 ) ) ;
#29366=FACE_OUTER_BOUND ( 'NONE', #16293, .T. ) ;
#29384=DIRECTION ( 'NONE',  ( 0.000000000000000000, 0.7071067811865475727, -0.7071067811865474617 ) ) ;
#29394=ORIENTED_EDGE ( 'NONE', *, *, #11681, .T. ) ;
#29416=LINE ( 'NONE', #1263, #38461 ) ;
#29418=DIRECTION ( 'NONE',  ( 0.000000000000000000, 0.000000000000000000, 1.000000000000000000 ) ) ;
#29428=CARTESIAN_POINT ( 'NONE',  ( -0.2746410161513779258, -3.985676108854518507, -0.7623095129438225426 ) ) ;
#29430=PRODUCT_DEFINITION_CONTEXT ( 'detailed design', #23728, 'design' ) ;
#29432=LINE ( 'NONE', #7612, #25169 ) ;
#29444=VERTEX_POINT ( 'NONE', #7575 ) ;
#29463=CARTESIAN_POINT ( 'NONE',  ( -0.2399999999999999079, -2.183180860297908144, -0.4937760292030871079 ) ) ;
#29472=DIRECTION ( 'NONE',  ( 0.000000000000000000, 0.000000000000000000, 1.000000000000000000 ) ) ;
#29479=ORIENTED_EDGE ( 'NONE', *, *, #5444, .F. ) ;
#29488=ORIENTED_EDGE ( 'NONE', *, *, #16129, .T. ) ;
#29495=DIRECTION ( 'NONE',  ( -1.000000000000000000, 0.000000000000000000, 0.000000000000000000 ) ) ;
#29498=ORIENTED_EDGE ( 'NONE', *, *, #29276, .T. ) ;
#29512=EDGE_CURVE ( 'NONE', #14911, #21211, #35724, .T. ) ;
#29514=DIRECTION ( 'NONE',  ( -0.4999999999999991118, 0.000000000000000000, 0.8660254037844391517 ) ) ;
#29545=CARTESIAN_POINT ( 'NONE',  ( -0.2399999999999999079, -2.231697337611688425, -0.6193912371520073901 ) ) ;
#29560=CARTESIAN_POINT ( 'NONE',  ( -0.3000000000000000999, -3.747168848490688209, -0.4747258284076885104 ) ) ;
#29567=DIRECTION ( 'NONE',  ( 0.000000000000000000, 0.000000000000000000, -1.000000000000000000 ) ) ;
#29578=DIRECTION ( 'NONE',  ( 0.000000000000000000, 0.000000000000000000, -1.000000000000000000 ) ) ;
#29581=ORIENTED_EDGE ( 'NONE', *, *, #19111, .T. ) ;
#29611=CARTESIAN_POINT ( 'NONE',  ( -0.2399999999999999079, -2.425196952834860920, -0.6298687015330038941 ) ) ;
#29616=DIRECTION ( 'NONE',  ( 0.000000000000000000, 0.000000000000000000, -1.000000000000000000 ) ) ;
#29626=VECTOR ( 'NONE', #34179, 39.37007874015748854 ) ;
#29633=ORIENTED_EDGE ( 'NONE', *, *, #15748, .T. ) ;
#29642=ORIENTED_EDGE ( 'NONE', *, *, #9029, .T. ) ;
#29646=FACE_OUTER_BOUND ( 'NONE', #28803, .T. ) ;
#29653=VECTOR ( 'NONE', #8624, 39.37007874015748143 ) ;
#29681=CIRCLE ( 'NONE', #36247, 0.4615209409081865166 ) ;
#29692=ORIENTED_EDGE ( 'NONE', *, *, #36555, .F. ) ;
#29709=AXIS2_PLACEMENT_3D ( 'NONE', #9420, #8816, #37399 ) ;
#29713=VECTOR ( 'NONE', #17911, 39.37007874015748143 ) ;
#29726=ORIENTED_EDGE ( 'NONE', *, *, #20784, .F. ) ;
#29734=CIRCLE ( 'NONE', #23181, 0.03999999999999930000 ) ;
#29740=CARTESIAN_POINT ( 'NONE',  ( -0.2399999999999999079, -3.849534981189179028, -0.1910928155360645808 ) ) ;
#29774=EDGE_CURVE ( 'NONE', #10935, #31618, #10609, .T. ) ;
#29781=AXIS2_PLACEMENT_3D ( 'NONE', #3771, #23924, #1727 ) ;
#29789=EDGE_LOOP ( 'NONE', ( #29726, #36153, #13181, #23292 ) ) ;
#29790=CARTESIAN_POINT ( 'NONE',  ( -0.2399999999999999079, -3.745280840418592661, 0.04438736989695814261 ) ) ;
#29799=CARTESIAN_POINT ( 'NONE',  ( -0.2399999999999999079, -2.409101312171279208, -0.6551853038253486750 ) ) ;
#29800=ORIENTED_EDGE ( 'NONE', *, *, #25521, .T. ) ;
#29815=DIRECTION ( 'NONE',  ( -1.000000000000000000, -0.000000000000000000, -0.000000000000000000 ) ) ;
#29833=EDGE_CURVE ( 'NONE', #19999, #1199, #31820, .T. ) ;
#29834=FACE_OUTER_BOUND ( 'NONE', #13988, .T. ) ;
#29836=CONICAL_SURFACE ( 'NONE', #12100, 0.1600000000000006140, 1.047197551196598075 ) ;
#29841=AXIS2_PLACEMENT_3D ( 'NONE', #15950, #9576, #28104 ) ;
#29844=AXIS2_PLACEMENT_3D ( 'NONE', #14374, #16669, #35583 ) ;
#29863=ORIENTED_EDGE ( 'NONE', *, *, #10636, .F. ) ;
#29879=CARTESIAN_POINT ( 'NONE',  ( -0.2746410161513776482, -3.838583118162426810, -0.3058907208964237734 ) ) ;
#29929=AXIS2_PLACEMENT_3D ( 'NONE', #17819, #14949, #40232 ) ;
#29930=CARTESIAN_POINT ( 'NONE',  ( -0.2746410161513770931, -2.945416957892569521, -0.4639726661791638840 ) ) ;
#29945=FACE_OUTER_BOUND ( 'NONE', #28753, .T. ) ;
#29969=LINE ( 'NONE', #23799, #21357 ) ;
#29977=EDGE_LOOP ( 'NONE', ( #8888, #12626, #33131, #36258 ) ) ;
#29978=CARTESIAN_POINT ( 'NONE',  ( -0.2746410161513779258, -2.154189217240303655, -0.3012881438978375903 ) ) ;
#29987=PLANE ( 'NONE',  #11359 ) ;
#30001=FACE_OUTER_BOUND ( 'NONE', #14892, .T. ) ;
#30021=ADVANCED_FACE ( 'NONE', ( #23786 ), #17375, .F. ) ;
#30022=FACE_OUTER_BOUND ( 'NONE', #34140, .T. ) ;
#30049=ORIENTED_EDGE ( 'NONE', *, *, #35301, .F. ) ;
#30061=LINE ( 'NONE', #4946, #6216 ) ;
#30099=CARTESIAN_POINT ( 'NONE',  ( -0.2746410161513782033, -1.739646749720735741, -0.3661865639197241507 ) ) ;
#30132=DIRECTION ( 'NONE',  ( 0.000000000000000000, 0.000000000000000000, -1.000000000000000000 ) ) ;
#30136=DIRECTION ( 'NONE',  ( 0.000000000000000000, 0.000000000000000000, 1.000000000000000000 ) ) ;
#30145=ORIENTED_EDGE ( 'NONE', *, *, #34387, .T. ) ;
#30157=EDGE_CURVE ( 'NONE', #35716, #38935, #23952, .T. ) ;
#30176=DIRECTION ( 'NONE',  ( -0.5000000000000000000, 0.8658613382927408120, -0.01685653730467018968 ) ) ;
#30198=ORIENTED_EDGE ( 'NONE', *, *, #32004, .F. ) ;
#30200=ORIENTED_EDGE ( 'NONE', *, *, #35301, .T. ) ;
#30217=DIRECTION ( 'NONE',  ( 0.000000000000000000, 0.000000000000000000, 1.000000000000000000 ) ) ;
#30231=ORIENTED_EDGE ( 'NONE', *, *, #34083, .F. ) ;
#30236=ORIENTED_EDGE ( 'NONE', *, *, #30843, .F. ) ;
#30238=FACE_OUTER_BOUND ( 'NONE', #16694, .T. ) ;
#30239=EDGE_LOOP ( 'NONE', ( #25601, #1300, #2632, #6258, #3383 ) ) ;
#30245=LINE ( 'NONE', #24113, #25320 ) ;
#30257=CARTESIAN_POINT ( 'NONE',  ( -0.2746410161513782033, -2.377058624452622393, -0.8919706583825134372 ) ) ;
#30268=EDGE_CURVE ( 'NONE', #38406, #24406, #23354, .T. ) ;
#30275=EDGE_CURVE ( 'NONE', #6266, #31712, #6205, .T. ) ;
#30313=ORIENTED_EDGE ( 'NONE', *, *, #26141, .T. ) ;
#30314=LINE ( 'NONE', #11611, #6193 ) ;
#30329=VECTOR ( 'NONE', #18875, 39.37007874015748854 ) ;
#30339=DIRECTION ( 'NONE',  ( 1.000000000000000000, 0.000000000000000000, 0.000000000000000000 ) ) ;
#30340=EDGE_CURVE ( 'NONE', #33790, #38637, #33578, .T. ) ;
#30348=EDGE_CURVE ( 'NONE', #9095, #9331, #95, .T. ) ;
#30356=EDGE_CURVE ( 'NONE', #17560, #11732, #23301, .T. ) ;
#30375=CARTESIAN_POINT ( 'NONE',  ( -0.2399999999999999079, -1.804235510932644004, -0.1101860188971505033 ) ) ;
#30389=DIRECTION ( 'NONE',  ( 0.000000000000000000, 0.5365213554527478168, -0.8438867430782083234 ) ) ;
#30391=VECTOR ( 'NONE', #25960, 39.37007874015748854 ) ;
#30397=ORIENTED_EDGE ( 'NONE', *, *, #11458, .T. ) ;
#30407=ORIENTED_EDGE ( 'NONE', *, *, #40466, .F. ) ;
#30423=DIRECTION ( 'NONE',  ( -1.000000000000000000, -0.000000000000000000, -0.000000000000000000 ) ) ;
#30431=CONICAL_SURFACE ( 'NONE', #12786, 0.5515209409081859304, 1.047197551196598519 ) ;
#30445=CARTESIAN_POINT ( 'NONE',  ( -0.2399999999999999079, -3.985676108854518507, -0.6623095129438225648 ) ) ;
#30446=CARTESIAN_POINT ( 'NONE',  ( -0.2746410161513779258, -2.416006048095809877, -1.059240699271965402 ) ) ;
#30452=EDGE_LOOP ( 'NONE', ( #7820, #17989, #20045, #21055 ) ) ;
#30476=CARTESIAN_POINT ( 'NONE',  ( -0.3000000000000000999, -2.891403747035983240, -0.7012825271972917829 ) ) ;
#30501=CARTESIAN_POINT ( 'NONE',  ( -0.2399999999999999079, -3.709638442894640509, -0.03148515058508863373 ) ) ;
#30508=AXIS2_PLACEMENT_3D ( 'NONE', #36059, #32762, #4564 ) ;
#30509=VECTOR ( 'NONE', #20100, 39.37007874015748143 ) ;
#30520=AXIS2_PLACEMENT_3D ( 'NONE', #10266, #34537, #37831 ) ;
#30533=AXIS2_PLACEMENT_3D ( 'NONE', #10517, #4534, #32925 ) ;
#30535=AXIS2_PLACEMENT_3D ( 'NONE', #19302, #29156, #6332 ) ;
#30546=FACE_OUTER_BOUND ( 'NONE', #4072, .T. ) ;
#30548=DIRECTION ( 'NONE',  ( 0.000000000000000000, 0.000000000000000000, -1.000000000000000000 ) ) ;
#30565=ORIENTED_EDGE ( 'NONE', *, *, #14108, .T. ) ;
#30582=CIRCLE ( 'NONE', #4955, 0.1346589359789737705 ) ;
#30596=CARTESIAN_POINT ( 'NONE',  ( -0.2399999999999999079, -2.139295658456680904, -0.2024034539465678073 ) ) ;
#30597=CARTESIAN_POINT ( 'NONE',  ( -0.2399999999999999079, -2.183180860297908144, -0.4937760292030871079 ) ) ;
#30602=DIRECTION ( 'NONE',  ( 1.000000000000000000, -0.000000000000000000, -0.000000000000000000 ) ) ;
#30612=CARTESIAN_POINT ( 'NONE',  ( -0.2399999999999999079, -3.941790907013290823, 0.08058400322088296597 ) ) ;
#30651=CARTESIAN_POINT ( 'NONE',  ( -0.2399999999999999079, -2.393162167644017124, -1.003759557197343888 ) ) ;
#30654=CARTESIAN_POINT ( 'NONE',  ( -0.2399999999999999079, -2.511040369707300268, -0.4948468226404901804 ) ) ;
#30655=AXIS2_PLACEMENT_3D ( 'NONE', #1228, #25907, #10865 ) ;
#30657=ORIENTED_EDGE ( 'NONE', *, *, #3848, .F. ) ;
#30662=DIRECTION ( 'NONE',  ( -1.000000000000000000, 0.000000000000000000, 0.000000000000000000 ) ) ;
#30663=DIRECTION ( 'NONE',  ( -0.5000000000000003331, -0.6415696268731877483, -0.5817116243241130524 ) ) ;
#30666=CIRCLE ( 'NONE', #8988, 0.1599999999999999201 ) ;
#30673=CARTESIAN_POINT ( 'NONE',  ( -0.2746410161513776482, -4.289222312108804225, -0.5708809693675255259 ) ) ;
#30705=LINE ( 'NONE', #33783, #29626 ) ;
#30712=ORIENTED_EDGE ( 'NONE', *, *, #34699, .F. ) ;
#30714=FACE_OUTER_BOUND ( 'NONE', #15790, .T. ) ;
#30750=EDGE_CURVE ( 'NONE', #8991, #22855, #23507, .T. ) ;
#30790=ADVANCED_FACE ( 'NONE', ( #8031 ), #8243, .F. ) ;
#30792=CARTESIAN_POINT ( 'NONE',  ( -0.3000000000000000999, -1.804235510932644004, -0.1501860188971498311 ) ) ;
#30821=CARTESIAN_POINT ( 'NONE',  ( -0.2746410161513779258, -1.730153431576819445, -0.08301574631829780615 ) ) ;
#30840=EDGE_CURVE ( 'NONE', #23694, #24904, #30245, .T. ) ;
#30843=EDGE_CURVE ( 'NONE', #8621, #2786, #35148, .T. ) ;
#30852=CARTESIAN_POINT ( 'NONE',  ( -0.3000000000000000999, -3.849534981189179028, -0.1910928155360645808 ) ) ;
#30866=CARTESIAN_POINT ( 'NONE',  ( -0.2399999999999999079, -1.948886540192243055, -0.2806949125330161499 ) ) ;
#30870=EDGE_CURVE ( 'NONE', #24980, #14090, #5763, .T. ) ;
#30872=DIRECTION ( 'NONE',  ( -1.000000000000000000, -0.000000000000000000, -0.000000000000000000 ) ) ;
#30876=DIRECTION ( 'NONE',  ( 0.000000000000000000, 0.000000000000000000, -1.000000000000000000 ) ) ;
#30880=DIRECTION ( 'NONE',  ( 0.4379975771764401671, 0.000000000000000000, -0.8989761522907980806 ) ) ;
#30896=CARTESIAN_POINT ( 'NONE',  ( -0.2746410161513779258, -1.874946189051298617, -0.07947534077849521816 ) ) ;
#30939=VERTEX_POINT ( 'NONE', #11551 ) ;
#30965=CARTESIAN_POINT ( 'NONE',  ( -0.2746410161513770931, -2.768941938641841904, -0.5551618215276493684 ) ) ;
#30966=CARTESIAN_POINT ( 'NONE',  ( -0.2399999999999999079, -2.811755946567116471, -0.3200729990151718884 ) ) ;
#30978=CIRCLE ( 'NONE', #13145, 0.1346589359789737705 ) ;
#30980=CIRCLE ( 'NONE', #29011, 0.1946589359789743512 ) ;
#30991=ORIENTED_EDGE ( 'NONE', *, *, #19248, .F. ) ;
#30998=ORIENTED_EDGE ( 'NONE', *, *, #35685, .F. ) ;
#31008=DIRECTION ( 'NONE',  ( 0.4999999999999996114, 0.000000000000000000, -0.8660254037844388186 ) ) ;
#31016=EDGE_CURVE ( 'NONE', #16220, #25252, #12151, .T. ) ;
#31051=LINE ( 'NONE', #11722, #7448 ) ;
#31054=VERTEX_POINT ( 'NONE', #6564 ) ;
#31093=VECTOR ( 'NONE', #17067, 39.37007874015748143 ) ;
#31098=VECTOR ( 'NONE', #14759, 39.37007874015748854 ) ;
#31107=VECTOR ( 'NONE', #4516, 39.37007874015748854 ) ;
#31108=VECTOR ( 'NONE', #29514, 39.37007874015748854 ) ;
#31109=ORIENTED_EDGE ( 'NONE', *, *, #13667, .F. ) ;
#31110=CARTESIAN_POINT ( 'NONE',  ( -0.3000000000000000999, -2.407646569606659792, -0.8438593182631384249 ) ) ;
#31111=ORIENTED_EDGE ( 'NONE', *, *, #35593, .F. ) ;
#31119=EDGE_LOOP ( 'NONE', ( #12388, #36017 ) ) ;
#31153=EDGE_CURVE ( 'NONE', #36582, #27000, #18733, .T. ) ;
#31165=DIRECTION ( 'NONE',  ( 0.000000000000000000, 0.000000000000000000, -1.000000000000000000 ) ) ;
#31172=ORIENTED_EDGE ( 'NONE', *, *, #14108, .F. ) ;
#31189=EDGE_CURVE ( 'NONE', #34622, #20383, #28570, .T. ) ;
#31197=AXIS2_PLACEMENT_3D ( 'NONE', #37519, #22528, #34451 ) ;
#31215=VECTOR ( 'NONE', #38700, 39.37007874015748143 ) ;
#31217=DIRECTION ( 'NONE',  ( 0.000000000000000000, 0.000000000000000000, -1.000000000000000000 ) ) ;
#31218=EDGE_CURVE ( 'NONE', #24904, #26308, #8349, .T. ) ;
#31239=LINE ( 'NONE', #40059, #2037 ) ;
#31242=ORIENTED_EDGE ( 'NONE', *, *, #29512, .F. ) ;
#31250=CIRCLE ( 'NONE', #19416, 0.1000000000000000194 ) ;
#31253=DIRECTION ( 'NONE',  ( 0.4999999999999972244, 0.7066258520834661772, 0.5006794435238159924 ) ) ;
#31298=EDGE_CURVE ( 'NONE', #36573, #29082, #29969, .T. ) ;
#31317=CARTESIAN_POINT ( 'NONE',  ( -0.2746410161513776482, -2.809880844172510272, -0.2480969101616946892 ) ) ;
#31323=CARTESIAN_POINT ( 'NONE',  ( -0.2399999999999999079, -2.425196952834860475, -0.6298687015330044492 ) ) ;
#31353=CARTESIAN_POINT ( 'NONE',  ( -0.2399999999999999079, -4.134278792318540674, -0.4999285807449073693 ) ) ;
#31356=LINE ( 'NONE', #37711, #38256 ) ;
#31367=ADVANCED_FACE ( 'NONE', ( #34246 ), #361, .F. ) ;
#31369=ORIENTED_EDGE ( 'NONE', *, *, #8544, .F. ) ;
#31371=EDGE_CURVE ( 'NONE', #34187, #34796, #34051, .T. ) ;
#31399=DIRECTION ( 'NONE',  ( 0.000000000000000000, 0.000000000000000000, -1.000000000000000000 ) ) ;
#31406=CARTESIAN_POINT ( 'NONE',  ( -0.2399999999999999079, -3.747168848490688209, -0.4747258284076885104 ) ) ;
#31411=DIRECTION ( 'NONE',  ( 0.000000000000000000, 0.000000000000000000, -1.000000000000000000 ) ) ;
#31419=DIRECTION ( 'NONE',  ( 1.000000000000000000, 0.000000000000000000, 0.000000000000000000 ) ) ;
#31443=FACE_BOUND ( 'NONE', #13133, .T. ) ;
#31500=CARTESIAN_POINT ( 'NONE',  ( -0.3000000000000000999, -2.511040369707300268, -0.5948468226404902692 ) ) ;
#31509=ORIENTED_EDGE ( 'NONE', *, *, #27739, .F. ) ;
#31510=ORIENTED_EDGE ( 'NONE', *, *, #11241, .T. ) ;
#31523=ORIENTED_EDGE ( 'NONE', *, *, #3621, .F. ) ;
#31528=CARTESIAN_POINT ( 'NONE',  ( -0.2399999999999999079, -3.384162466027138105, -0.4389494074304161608 ) ) ;
#31540=DIRECTION ( 'NONE',  ( 0.4999999999999991118, 0.2433878240179132291, 0.8311211506873266153 ) ) ;
#31554=VECTOR ( 'NONE', #19386, 39.37007874015748854 ) ;
#31561=CARTESIAN_POINT ( 'NONE',  ( -0.2399999999999999079, -3.094053300116982985, 0.06803269733885447534 ) ) ;
#31562=EDGE_LOOP ( 'NONE', ( #5716, #2548, #2887, #36081 ) ) ;
#31563=EDGE_LOOP ( 'NONE', ( #651, #9816, #31369, #33687 ) ) ;
#31604=LINE ( 'NONE', #31814, #30329 ) ;
#31611=DIRECTION ( 'NONE',  ( 0.000000000000000000, 0.000000000000000000, -1.000000000000000000 ) ) ;
#31615=FACE_OUTER_BOUND ( 'NONE', #7528, .T. ) ;
#31618=VERTEX_POINT ( 'NONE', #23096 ) ;
#31620=CIRCLE ( 'NONE', #27604, 0.1000000000000000194 ) ;
#31621=DIRECTION ( 'NONE',  ( 0.000000000000000000, 0.000000000000000000, -1.000000000000000000 ) ) ;
#31622=VERTEX_POINT ( 'NONE', #7217 ) ;
#31633=DIRECTION ( 'NONE',  ( 0.000000000000000000, 0.000000000000000000, -1.000000000000000000 ) ) ;
#31648=DIRECTION ( 'NONE',  ( 1.000000000000000000, 0.000000000000000000, 0.000000000000000000 ) ) ;
#31662=EDGE_CURVE ( 'NONE', #1392, #7421, #1066, .T. ) ;
#31687=VECTOR ( 'NONE', #22099, 39.37007874015748143 ) ;
#31712=VERTEX_POINT ( 'NONE', #25945 ) ;
#31716=DIRECTION ( 'NONE',  ( 1.000000000000000000, 0.000000000000000000, 0.000000000000000000 ) ) ;
#31721=LINE ( 'NONE', #37900, #9357 ) ;
#31755=DIRECTION ( 'NONE',  ( 1.000000000000000000, 0.000000000000000000, 0.000000000000000000 ) ) ;
#31760=EDGE_CURVE ( 'NONE', #27450, #20248, #6382, .T. ) ;
#31762=ORIENTED_EDGE ( 'NONE', *, *, #37528, .T. ) ;
#31767=CONICAL_SURFACE ( 'NONE', #8769, 0.1600000000000006140, 1.047197551196599630 ) ;
#31774=ORIENTED_EDGE ( 'NONE', *, *, #6586, .F. ) ;
#31781=VECTOR ( 'NONE', #17282, 39.37007874015748143 ) ;
#31801=VECTOR ( 'NONE', #5426, 39.37007874015748143 ) ;
#31810=VECTOR ( 'NONE', #21897, 39.37007874015748143 ) ;
#31811=EDGE_LOOP ( 'NONE', ( #24212, #29642, #4877, #30198, #34748 ) ) ;
#31814=CARTESIAN_POINT ( 'NONE',  ( -0.3000000000000000999, -2.461298705151934829, -0.7594706439553173816 ) ) ;
#31817=ADVANCED_FACE ( 'NONE', ( #19743 ), #12767, .F. ) ;
#31820=LINE ( 'NONE', #25870, #14699 ) ;
#31822=EDGE_CURVE ( 'NONE', #26475, #8991, #31250, .T. ) ;
#31824=DIRECTION ( 'NONE',  ( -0.4379975771764391679, 0.8989761522907986357, 0.000000000000000000 ) ) ;
#31833=VECTOR ( 'NONE', #20372, 39.37007874015748854 ) ;
#31871=EDGE_LOOP ( 'NONE', ( #4334, #27534, #19504, #3535 ) ) ;
#31893=AXIS2_PLACEMENT_3D ( 'NONE', #29879, #7437, #39135 ) ;
#31915=CLOSED_SHELL ( 'NONE', ( #15192, #40468, #21538, #1768, #30021, #706, #13018, #28141, #17026, #8970, #18247, #22292, #26655, #34063, #19535, #24259, #29151, #6246, #17971, #24279, #39407, #12279, #27618, #32289, #16228, #8400, #2528, #14310, #18735, #18538, #29020, #9286, #13435, #21479, #19025, #13992, #18533, #4414, #18816, #23534, #6699, #13644, #35150, #3776, #13446, #10933, #31367, #35912, #34316, #37056, #20968, #32312, #22745, #7521, #24355, #7669, #39685, #5715, #34698, #30790, #28777, #26588, #35649, #25291, #15011, #11617, #26613, #20054, #19975, #16102, #34659, #37644, #37985, #19473, #34879, #9183, #4863, #22121, #654, #24, #21013, #10136, #19482, #25121, #40037, #35647, #38554, #39632, #7933, #32162, #15851, #10760, #7758, #19052, #37102, #3327, #34041, #13238, #3681, #8627, #16800, #12020, #13534, #19746, #9160, #31817, #7714, #38474, #535, #22534, #7883, #26272, #32384, #38076, #37921, #35944, #27308, #36312, #37084, #12418, #33003, #23603, #5195, #26936, #8452, #33299 ) ) ;
#31920=VERTEX_POINT ( 'NONE', #32484 ) ;
#31927=ORIENTED_EDGE ( 'NONE', *, *, #24249, .F. ) ;
#31928=EDGE_CURVE ( 'NONE', #23895, #34187, #6903, .T. ) ;
#31960=DIRECTION ( 'NONE',  ( 1.000000000000000000, 0.000000000000000000, 0.000000000000000000 ) ) ;
#31972=DIRECTION ( 'NONE',  ( 1.000000000000000000, -0.000000000000000000, -0.000000000000000000 ) ) ;
#31983=VECTOR ( 'NONE', #18901, 39.37007874015748143 ) ;
#31996=CARTESIAN_POINT ( 'NONE',  ( -0.2399999999999999079, -2.294529520598973082, -0.6534431116140350104 ) ) ;
#31999=CARTESIAN_POINT ( 'NONE',  ( -0.3000000000000000999, -3.941790907013290823, -0.009415996779116623042 ) ) ;
#32004=EDGE_CURVE ( 'NONE', #33731, #36543, #29416, .T. ) ;
#32008=DIRECTION ( 'NONE',  ( 0.000000000000000000, 0.000000000000000000, -1.000000000000000000 ) ) ;
#32026=CARTESIAN_POINT ( 'NONE',  ( -0.2746410161513779258, -2.511040369707300268, -0.4948468226404901804 ) ) ;
#32045=DIRECTION ( 'NONE',  ( 0.000000000000000000, 0.000000000000000000, -1.000000000000000000 ) ) ;
#32088=ORIENTED_EDGE ( 'NONE', *, *, #14683, .F. ) ;
#32090=FACE_OUTER_BOUND ( 'NONE', #4942, .T. ) ;
#32100=DIRECTION ( 'NONE',  ( 1.000000000000000000, 0.000000000000000000, 0.000000000000000000 ) ) ;
#32129=DIRECTION ( 'NONE',  ( 1.000000000000000000, -0.000000000000000000, -0.000000000000000000 ) ) ;
#32162=ADVANCED_FACE ( 'NONE', ( #33929 ), #24679, .T. ) ;
#32167=CARTESIAN_POINT ( 'NONE',  ( -0.2399999999999999079, -2.139295658456680904, -0.2024034539465678073 ) ) ;
#32168=ORIENTED_EDGE ( 'NONE', *, *, #9491, .T. ) ;
#32200=FACE_OUTER_BOUND ( 'NONE', #2817, .T. ) ;
#32214=CARTESIAN_POINT ( 'NONE',  ( -0.2399999999999999079, -3.941790907013290823, -0.2762780017083287243 ) ) ;
#32221=CIRCLE ( 'NONE', #9228, 0.1000000000000000194 ) ;
#32222=CARTESIAN_POINT ( 'NONE',  ( -0.2399999999999999079, -3.667123564397057667, -0.3682398926280779361 ) ) ;
#32224=ORIENTED_EDGE ( 'NONE', *, *, #24249, .T. ) ;
#32227=VECTOR ( 'NONE', #38281, 39.37007874015748854 ) ;
#32239=CARTESIAN_POINT ( 'NONE',  ( -0.2399999999999999079, -3.941790907013290823, -0.4709369376873030477 ) ) ;
#32240=CARTESIAN_POINT ( 'NONE',  ( -0.2399999999999999079, -3.812085038045152974, -0.02801711824816583915 ) ) ;
#32241=CARTESIAN_POINT ( 'NONE',  ( -0.3000000000000000999, -2.183180860297908144, -0.5562760292030870524 ) ) ;
#32248=ORIENTED_EDGE ( 'NONE', *, *, #33306, .F. ) ;
#32257=CARTESIAN_POINT ( 'NONE',  ( -0.2399999999999999079, -3.334889855281614857, -0.6641625420049475093 ) ) ;
#32258=ORIENTED_EDGE ( 'NONE', *, *, #5199, .T. ) ;
#32269=LINE ( 'NONE', #473, #22772 ) ;
#32276=DIRECTION ( 'NONE',  ( -0.8660254037844415942, 0.4219433715391002759, 0.2682606777263707998 ) ) ;
#32286=CARTESIAN_POINT ( 'NONE',  ( -0.2399999999999999079, -2.289343986263487896, -0.7686455968847020204 ) ) ;
#32287=VECTOR ( 'NONE', #34165, 39.37007874015748854 ) ;
#32289=ADVANCED_FACE ( 'NONE', ( #18906, #38014, #22395, #31443, #3250, #620 ), #12507, .F. ) ;
#32296=DIRECTION ( 'NONE',  ( 0.4999999999999973910, -0.8563665354314760059, -0.1289820025937470083 ) ) ;
#32308=ORIENTED_EDGE ( 'NONE', *, *, #18050, .T. ) ;
#32309=ORIENTED_EDGE ( 'NONE', *, *, #26778, .F. ) ;
#32312=ADVANCED_FACE ( 'NONE', ( #28347 ), #13114, .T. ) ;
#32313=CIRCLE ( 'NONE', #40182, 0.1000000000000000194 ) ;
#32315=CARTESIAN_POINT ( 'NONE',  ( -0.2399999999999999079, -2.646062248599815092, -0.5806902395129298622 ) ) ;
#32337=EDGE_CURVE ( 'NONE', #39872, #2349, #37236, .T. ) ;
#32345=CONICAL_SURFACE ( 'NONE', #14605, 0.1600000000000004197, 1.047197551196596743 ) ;
#32360=ORIENTED_EDGE ( 'NONE', *, *, #9486, .T. ) ;
#32364=EDGE_CURVE ( 'NONE', #4884, #6766, #39912, .T. ) ;
#32367=DIRECTION ( 'NONE',  ( 0.000000000000000000, 0.000000000000000000, -1.000000000000000000 ) ) ;
#32375=VERTEX_POINT ( 'NONE', #9053 ) ;
#32376=EDGE_CURVE ( 'NONE', #32724, #19429, #15853, .T. ) ;
#32380=VECTOR ( 'NONE', #13125, 39.37007874015748143 ) ;
#32384=ADVANCED_FACE ( 'NONE', ( #27172 ), #5133, .F. ) ;
#32396=EDGE_LOOP ( 'NONE', ( #21165, #25476, #11174, #5141 ) ) ;
#32400=CIRCLE ( 'NONE', #8087, 0.1000000000000000194 ) ;
#32402=EDGE_LOOP ( 'NONE', ( #12845, #11690, #17188, #39203 ) ) ;
#32407=AXIS2_PLACEMENT_3D ( 'NONE', #9433, #38425, #35152 ) ;
#32417=EDGE_CURVE ( 'NONE', #24392, #33731, #31620, .T. ) ;
#32423=EDGE_LOOP ( 'NONE', ( #22280, #17359, #14174, #5394 ) ) ;
#32441=DIRECTION ( 'NONE',  ( 1.000000000000000000, 0.000000000000000000, 0.000000000000000000 ) ) ;
#32461=CARTESIAN_POINT ( 'NONE',  ( -0.2399999999999999079, -3.941790907013290823, -0.4709369376873030477 ) ) ;
#32468=ORIENTED_EDGE ( 'NONE', *, *, #25580, .T. ) ;
#32473=CONICAL_SURFACE ( 'NONE', #983, 0.1600000000000015854, 1.047197551196600518 ) ;
#32484=CARTESIAN_POINT ( 'NONE',  ( -0.3000000000000000999, -2.342996121808762044, -0.6842569225768811991 ) ) ;
#32489=AXIS2_PLACEMENT_3D ( 'NONE', #10482, #10303, #35384 ) ;
#32490=CIRCLE ( 'NONE', #10839, 0.1600000000000015854 ) ;
#32495=LINE ( 'NONE', #7386, #20072 ) ;
#32500=EDGE_CURVE ( 'NONE', #26308, #9095, #796, .T. ) ;
#32512=ORIENTED_EDGE ( 'NONE', *, *, #33305, .F. ) ;
#32531=ORIENTED_EDGE ( 'NONE', *, *, #17074, .T. ) ;
#32534=AXIS2_PLACEMENT_3D ( 'NONE', #1081, #28818, #10911 ) ;
#32540=FACE_OUTER_BOUND ( 'NONE', #15365, .T. ) ;
#32557=EDGE_CURVE ( 'NONE', #24814, #38935, #25767, .T. ) ;
#32560=EDGE_CURVE ( 'NONE', #17501, #22855, #32838, .T. ) ;
#32569=ORIENTED_EDGE ( 'NONE', *, *, #8878, .T. ) ;
#32575=ORIENTED_EDGE ( 'NONE', *, *, #3993, .F. ) ;
#32591=ORIENTED_EDGE ( 'NONE', *, *, #6908, .F. ) ;
#32592=VERTEX_POINT ( 'NONE', #37518 ) ;
#32605=EDGE_CURVE ( 'NONE', #9809, #23695, #8778, .T. ) ;
#32614=ORIENTED_EDGE ( 'NONE', *, *, #32004, .T. ) ;
#32628=DIRECTION ( 'NONE',  ( 0.5000000000000009992, -0.7308273574226400449, -0.4646411234949396341 ) ) ;
#32644=AXIS2_PLACEMENT_3D ( 'NONE', #22511, #31960, #22923 ) ;
#32648=DIRECTION ( 'NONE',  ( -1.000000000000000000, 0.000000000000000000, 0.000000000000000000 ) ) ;
#32693=DIRECTION ( 'NONE',  ( 0.000000000000000000, 0.000000000000000000, -1.000000000000000000 ) ) ;
#32695=DIRECTION ( 'NONE',  ( 0.000000000000000000, 0.000000000000000000, -1.000000000000000000 ) ) ;
#32714=ORIENTED_EDGE ( 'NONE', *, *, #5418, .T. ) ;
#32720=VERTEX_POINT ( 'NONE', #32315 ) ;
#32722=ORIENTED_EDGE ( 'NONE', *, *, #9934, .T. ) ;
#32724=VERTEX_POINT ( 'NONE', #15113 ) ;
#32727=CARTESIAN_POINT ( 'NONE',  ( -0.2399999999999999079, -1.906460133321048911, -0.3231213194042101278 ) ) ;
#32744=CARTESIAN_POINT ( 'NONE',  ( -0.3000000000000000999, -3.758594918004649621, -0.06617323996463200797 ) ) ;
#32749=CARTESIAN_POINT ( 'NONE',  ( -0.2746410161513776482, -3.941790907013290823, -0.2762780017083287243 ) ) ;
#32762=DIRECTION ( 'NONE',  ( -0.8660254037844402619, 0.4079706259167340532, 0.2890674114961865326 ) ) ;
#32764=DIRECTION ( 'NONE',  ( 0.000000000000000000, 0.000000000000000000, -1.000000000000000000 ) ) ;
#32766=ORIENTED_EDGE ( 'NONE', *, *, #34569, .F. ) ;
#32777=EDGE_CURVE ( 'NONE', #14064, #28382, #38698, .T. ) ;
#32789=EDGE_CURVE ( 'NONE', #21211, #32720, #27853, .T. ) ;
#32801=DIRECTION ( 'NONE',  ( 0.8660254037844378194, -0.4079706259167369953, -0.2890674114961894747 ) ) ;
#32803=ORIENTED_EDGE ( 'NONE', *, *, #35438, .T. ) ;
#32814=DIRECTION ( 'NONE',  ( 1.000000000000000000, -0.000000000000000000, -0.000000000000000000 ) ) ;
#32816=LINE ( 'NONE', #33238, #30509 ) ;
#32817=CARTESIAN_POINT ( 'NONE',  ( -0.2399999999999999079, -3.285933380171606188, -0.6294744526254046901 ) ) ;
#32826=CARTESIAN_POINT ( 'NONE',  ( -0.2399999999999999079, -3.941790907013290823, -0.4084369376873030477 ) ) ;
#32828=EDGE_CURVE ( 'NONE', #38406, #19999, #29167, .T. ) ;
#32830=DIRECTION ( 'NONE',  ( 1.000000000000000000, -0.000000000000000000, -0.000000000000000000 ) ) ;
#32838=CIRCLE ( 'NONE', #36863, 0.1000000000000000194 ) ;
#32840=DIRECTION ( 'NONE',  ( -1.000000000000000000, 0.000000000000000000, 0.000000000000000000 ) ) ;
#32859=ORIENTED_EDGE ( 'NONE', *, *, #11943, .F. ) ;
#32862=CARTESIAN_POINT ( 'NONE',  ( -0.3000000000000000999, -1.874946189051298617, -0.07947534077849525980 ) ) ;
#32896=VECTOR ( 'NONE', #33798, 39.37007874015748143 ) ;
#32905=DIRECTION ( 'NONE',  ( 0.000000000000000000, 0.000000000000000000, -1.000000000000000000 ) ) ;
#32910=ORIENTED_EDGE ( 'NONE', *, *, #5936, .F. ) ;
#32918=VECTOR ( 'NONE', #39776, 39.37007874015748143 ) ;
#32925=DIRECTION ( 'NONE',  ( 0.000000000000000000, 0.000000000000000000, -1.000000000000000000 ) ) ;
#32937=VECTOR ( 'NONE', #36108, 39.37007874015748143 ) ;
#32943=CONICAL_SURFACE ( 'NONE', #19792, 0.1600000000000000588, 1.047197551196602738 ) ;
#32962=CIRCLE ( 'NONE', #35612, 0.1000000000000000194 ) ;
#32969=LINE ( 'NONE', #30099, #23237 ) ;
#33003=ADVANCED_FACE ( 'NONE', ( #5780 ), #27599, .F. ) ;
#33005=DIRECTION ( 'NONE',  ( 0.4999999999999973910, -0.6123724356957970238, 0.6123724356957940262 ) ) ;
#33035=CIRCLE ( 'NONE', #18598, 0.06250000000000001388 ) ;
#33074=DIRECTION ( 'NONE',  ( -1.000000000000000000, -0.000000000000000000, -0.000000000000000000 ) ) ;
#33087=AXIS2_PLACEMENT_3D ( 'NONE', #23031, #6972, #34954 ) ;
#33100=LINE ( 'NONE', #29611, #27067 ) ;
#33101=CARTESIAN_POINT ( 'NONE',  ( -0.3000000000000000999, -4.056386786973173564, -0.6915988348251679296 ) ) ;
#33105=CARTESIAN_POINT ( 'NONE',  ( -0.3000000000000000999, -3.237612445311622622, -0.5419983935656527141 ) ) ;
#33131=ORIENTED_EDGE ( 'NONE', *, *, #21482, .F. ) ;
#33134=VERTEX_POINT ( 'NONE', #3723 ) ;
#33159=VECTOR ( 'NONE', #11563, 39.37007874015748854 ) ;
#33160=DIRECTION ( 'NONE',  ( -1.000000000000000000, -0.000000000000000000, -0.000000000000000000 ) ) ;
#33177=AXIS2_PLACEMENT_3D ( 'NONE', #13498, #16577, #38582 ) ;
#33185=LINE ( 'NONE', #33381, #2204 ) ;
#33220=DIRECTION ( 'NONE',  ( -1.000000000000000000, -0.000000000000000000, -0.000000000000000000 ) ) ;
#33238=CARTESIAN_POINT ( 'NONE',  ( -0.3000000000000000999, -2.891403747035983240, -0.7012825271972917829 ) ) ;
#33255=DIRECTION ( 'NONE',  ( -0.4999999999999991673, 0.000000000000000000, 0.8660254037844391517 ) ) ;
#33259=CIRCLE ( 'NONE', #30655, 0.1600000000000006140 ) ;
#33268=CIRCLE ( 'NONE', #15545, 0.1000000000000000194 ) ;
#33298=LINE ( 'NONE', #5106, #39042 ) ;
#33299=ADVANCED_FACE ( 'NONE', ( #1268 ), #32473, .F. ) ;
#33303=EDGE_CURVE ( 'NONE', #36573, #4130, #9490, .T. ) ;
#33305=EDGE_CURVE ( 'NONE', #6106, #23675, #12115, .T. ) ;
#33306=EDGE_CURVE ( 'NONE', #7581, #27128, #19977, .T. ) ;
#33310=CARTESIAN_POINT ( 'NONE',  ( -0.2399999999999999079, -2.945416957892569521, -0.4639726661791638840 ) ) ;
#33327=DIRECTION ( 'NONE',  ( 1.000000000000000000, -0.000000000000000000, -0.000000000000000000 ) ) ;
#33366=EDGE_CURVE ( 'NONE', #27977, #7075, #25233, .T. ) ;
#33381=CARTESIAN_POINT ( 'NONE',  ( -0.2746410161513779258, -2.423474325126674156, -0.5576739111151495232 ) ) ;
#33408=CARTESIAN_POINT ( 'NONE',  ( -0.3000000000000000999, -4.250025578259899461, -0.8852376261118949374 ) ) ;
#33417=EDGE_CURVE ( 'NONE', #40610, #31712, #18293, .T. ) ;
#33422=VERTEX_POINT ( 'NONE', #8409 ) ;
#33424=PLANE ( 'NONE',  #35758 ) ;
#33434=CARTESIAN_POINT ( 'NONE',  ( -0.2746410161513776482, -3.730063144961804245, -0.1064410973704724706 ) ) ;
#33437=LINE ( 'NONE', #36931, #16523 ) ;
#33444=ORIENTED_EDGE ( 'NONE', *, *, #2953, .T. ) ;
#33448=DIRECTION ( 'NONE',  ( 0.000000000000000000, 0.000000000000000000, 1.000000000000000000 ) ) ;
#33460=DIRECTION ( 'NONE',  ( -1.000000000000000000, -0.000000000000000000, -0.000000000000000000 ) ) ;
#33462=CARTESIAN_POINT ( 'NONE',  ( -0.2399999999999999079, -2.289343986263487896, -0.7686455968847020204 ) ) ;
#33491=CARTESIAN_POINT ( 'NONE',  ( -0.2746410161513782033, -2.294529520598973082, -0.6534431116140350104 ) ) ;
#33517=DIRECTION ( 'NONE',  ( -0.8660254037844427044, -0.4079706259167306115, -0.2890674114961839236 ) ) ;
#33527=CARTESIAN_POINT ( 'NONE',  ( -0.2399999999999999079, -3.268524983732796318, -0.6433364877554561545 ) ) ;
#33543=CARTESIAN_POINT ( 'NONE',  ( -0.3000000000000000999, -2.183180860297908144, -0.4937760292030871079 ) ) ;
#33559=DIRECTION ( 'NONE',  ( 0.000000000000000000, 0.000000000000000000, -1.000000000000000000 ) ) ;
#33563=EDGE_CURVE ( 'NONE', #21137, #19197, #3559, .T. ) ;
#33564=AXIS2_PLACEMENT_3D ( 'NONE', #4996, #8684, #40157 ) ;
#33572=EDGE_LOOP ( 'NONE', ( #9963, #2581 ) ) ;
#33578=LINE ( 'NONE', #15278, #332 ) ;
#33599=DIRECTION ( 'NONE',  ( 0.8660254037844383745, 0.1781528605886715799, 0.4671847153579342660 ) ) ;
#33626=AXIS2_PLACEMENT_3D ( 'NONE', #18952, #40542, #37447 ) ;
#33642=EDGE_LOOP ( 'NONE', ( #30236, #1049, #11812, #34784 ) ) ;
#33644=DIRECTION ( 'NONE',  ( 1.000000000000000000, 0.000000000000000000, 0.000000000000000000 ) ) ;
#33665=VECTOR ( 'NONE', #35154, 39.37007874015748143 ) ;
#33666=VERTEX_POINT ( 'NONE', #15514 ) ;
#33670=CARTESIAN_POINT ( 'NONE',  ( -0.3000000000000000999, -1.962518963160043706, -0.3791801492432049780 ) ) ;
#33682=DIRECTION ( 'NONE',  ( 1.000000000000000000, 0.000000000000000000, 0.000000000000000000 ) ) ;
#33687=ORIENTED_EDGE ( 'NONE', *, *, #24325, .F. ) ;
#33695=VERTEX_POINT ( 'NONE', #8923 ) ;
#33696=ORIENTED_EDGE ( 'NONE', *, *, #9000, .T. ) ;
#33706=VECTOR ( 'NONE', #32296, 39.37007874015747433 ) ;
#33707=EDGE_CURVE ( 'NONE', #7421, #36854, #26565, .T. ) ;
#33713=( GEOMETRIC_REPRESENTATION_CONTEXT ( 3 ) GLOBAL_UNCERTAINTY_ASSIGNED_CONTEXT ( ( #18632 ) ) GLOBAL_UNIT_ASSIGNED_CONTEXT ( ( #324, #38110, #35637 ) ) REPRESENTATION_CONTEXT ( 'NONE', 'WORKASPACE' ) );
#33731=VERTEX_POINT ( 'NONE', #5819 ) ;
#33735=ORIENTED_EDGE ( 'NONE', *, *, #13417, .F. ) ;
#33751=LINE ( 'NONE', #9069, #2821 ) ;
#33757=AXIS2_PLACEMENT_3D ( 'NONE', #38234, #35366, #19928 ) ;
#33761=DIRECTION ( 'NONE',  ( 0.000000000000000000, 0.000000000000000000, -1.000000000000000000 ) ) ;
#33769=EDGE_CURVE ( 'NONE', #22735, #28470, #2752, .T. ) ;
#33783=CARTESIAN_POINT ( 'NONE',  ( -0.2746410161513779258, -2.377368549242099949, -0.4802393080720198104 ) ) ;
#33790=VERTEX_POINT ( 'NONE', #327 ) ;
#33798=DIRECTION ( 'NONE',  ( -0.4999999999999976685, 0.5006794435238191010, -0.7066258520834637347 ) ) ;
#33812=EDGE_LOOP ( 'NONE', ( #24381, #12628, #22238, #35917 ) ) ;
#33819=CARTESIAN_POINT ( 'NONE',  ( -0.2399999999999999079, -1.835749455202394298, -0.3938319975228649072 ) ) ;
#33820=AXIS2_PLACEMENT_3D ( 'NONE', #23602, #36117, #7924 ) ;
#33831=VECTOR ( 'NONE', #7636, 39.37007874015748854 ) ;
#33842=DIRECTION ( 'NONE',  ( -0.4709550870498656616, 0.000000000000000000, -0.8821571889305518388 ) ) ;
#33867=ORIENTED_EDGE ( 'NONE', *, *, #11878, .T. ) ;
#33868=DIRECTION ( 'NONE',  ( 1.000000000000000000, 0.000000000000000000, 0.000000000000000000 ) ) ;
#33873=EDGE_CURVE ( 'NONE', #6348, #35653, #28453, .T. ) ;
#33889=DIRECTION ( 'NONE',  ( -1.000000000000000000, -0.000000000000000000, -0.000000000000000000 ) ) ;
#33892=DIRECTION ( 'NONE',  ( -1.000000000000000000, -0.000000000000000000, -0.000000000000000000 ) ) ;
#33902=AXIS2_PLACEMENT_3D ( 'NONE', #7085, #19655, #16569 ) ;
#33906=LINE ( 'NONE', #5703, #20437 ) ;
#33914=CARTESIAN_POINT ( 'NONE',  ( -0.2399999999999999079, -3.849534981189179028, -0.3510928155360652503 ) ) ;
#33916=DIRECTION ( 'NONE',  ( -1.000000000000000000, -0.000000000000000000, -0.000000000000000000 ) ) ;
#33928=DIRECTION ( 'NONE',  ( 0.000000000000000000, -0.5781348229923771731, 0.8159412518334715481 ) ) ;
#33929=FACE_OUTER_BOUND ( 'NONE', #38088, .T. ) ;
#33959=ORIENTED_EDGE ( 'NONE', *, *, #7205, .T. ) ;
#33963=DIRECTION ( 'NONE',  ( 1.000000000000000000, -0.000000000000000000, -0.000000000000000000 ) ) ;
#33972=CYLINDRICAL_SURFACE ( 'NONE', #33626, 0.1000000000000000056 ) ;
#33979=DIRECTION ( 'NONE',  ( -1.000000000000000000, -0.000000000000000000, -0.000000000000000000 ) ) ;
#33986=FACE_OUTER_BOUND ( 'NONE', #32402, .T. ) ;
#34017=DIRECTION ( 'NONE',  ( 0.000000000000000000, 0.000000000000000000, -1.000000000000000000 ) ) ;
#34036=DIRECTION ( 'NONE',  ( 0.4999999999999995559, 0.6123724356957944703, -0.6123724356957950254 ) ) ;
#34041=ADVANCED_FACE ( 'NONE', ( #16928 ), #30431, .T. ) ;
#34047=VERTEX_POINT ( 'NONE', #39144 ) ;
#34051=LINE ( 'NONE', #9149, #19387 ) ;
#34063=ADVANCED_FACE ( 'NONE', ( #12568 ), #12371, .F. ) ;
#34064=DIRECTION ( 'NONE',  ( 0.000000000000000000, 0.000000000000000000, -1.000000000000000000 ) ) ;
#34077=DIRECTION ( 'NONE',  ( 0.000000000000000000, -0.7071067811865465735, -0.7071067811865484609 ) ) ;
#34082=ORIENTED_EDGE ( 'NONE', *, *, #39715, .F. ) ;
#34083=EDGE_CURVE ( 'NONE', #29082, #36582, #40284, .T. ) ;
#34085=CARTESIAN_POINT ( 'NONE',  ( -0.2399999999999999079, -4.320736256378554963, -0.8145269479932405465 ) ) ;
#34105=EDGE_LOOP ( 'NONE', ( #40326, #3052, #700, #946, #26856, #30991, #15844, #21916, #30657, #7500, #665, #21765, #29030, #36666, #1889, #13007, #12634, #5385, #31523, #5806, #9301, #22533, #28645, #17576, #5103, #17407, #127 ) ) ;
#34120=DIRECTION ( 'NONE',  ( 0.000000000000000000, 0.000000000000000000, -1.000000000000000000 ) ) ;
#34129=CYLINDRICAL_SURFACE ( 'NONE', #13359, 0.1000000000000000194 ) ;
#34140=EDGE_LOOP ( 'NONE', ( #8248, #18077, #596, #35282 ) ) ;
#34142=VERTEX_POINT ( 'NONE', #8877 ) ;
#34165=DIRECTION ( 'NONE',  ( 0.000000000000000000, 0.7071067811865474617, 0.7071067811865474617 ) ) ;
#34179=DIRECTION ( 'NONE',  ( 0.4999999999999983902, 0.8639288552672733656, -0.06022402374949849257 ) ) ;
#34187=VERTEX_POINT ( 'NONE', #284 ) ;
#34188=ORIENTED_EDGE ( 'NONE', *, *, #9692, .F. ) ;
#34203=ORIENTED_EDGE ( 'NONE', *, *, #17428, .F. ) ;
#34233=EDGE_LOOP ( 'NONE', ( #9664, #25311, #5838, #21966 ) ) ;
#34246=FACE_OUTER_BOUND ( 'NONE', #19825, .T. ) ;
#34275=CARTESIAN_POINT ( 'NONE',  ( -0.3000000000000000999, -2.853330612949663170, -0.6088139570729240724 ) ) ;
#34285=VECTOR ( 'NONE', #6005, 39.37007874015748143 ) ;
#34305=ORIENTED_EDGE ( 'NONE', *, *, #32364, .T. ) ;
#34316=ADVANCED_FACE ( 'NONE', ( #28774 ), #32, .T. ) ;
#34324=VECTOR ( 'NONE', #36814, 39.37007874015748854 ) ;
#34340=FACE_OUTER_BOUND ( 'NONE', #8998, .T. ) ;
#34359=DIRECTION ( 'NONE',  ( 0.000000000000000000, 0.8438867430782092116, 0.5365213554527465956 ) ) ;
#34361=DIRECTION ( 'NONE',  ( 1.000000000000000000, 0.000000000000000000, 0.000000000000000000 ) ) ;
#34368=EDGE_CURVE ( 'NONE', #26308, #26277, #28168, .T. ) ;
#34383=DIRECTION ( 'NONE',  ( 0.000000000000000000, -0.8438867430782093226, -0.5365213554527464845 ) ) ;
#34387=EDGE_CURVE ( 'NONE', #34142, #30939, #3585, .T. ) ;
#34389=ORIENTED_EDGE ( 'NONE', *, *, #7930, .F. ) ;
#34392=EDGE_CURVE ( 'NONE', #11216, #35098, #28573, .T. ) ;
#34401=EDGE_CURVE ( 'NONE', #10078, #34849, #11397, .T. ) ;
#34443=ORIENTED_EDGE ( 'NONE', *, *, #17925, .T. ) ;
#34446=ORIENTED_EDGE ( 'NONE', *, *, #40466, .T. ) ;
#34451=DIRECTION ( 'NONE',  ( 0.000000000000000000, 0.9343694307158671997, -0.3563057211773426602 ) ) ;
#34463=VECTOR ( 'NONE', #12392, 39.37007874015748854 ) ;
#34482=CARTESIAN_POINT ( 'NONE',  ( -0.2399999999999999079, -2.853330612949663170, -0.6088139570729240724 ) ) ;
#34487=DIRECTION ( 'NONE',  ( -1.000000000000000000, -0.000000000000000000, -0.000000000000000000 ) ) ;
#34489=VECTOR ( 'NONE', #9248, 39.37007874015748143 ) ;
#34495=ORIENTED_EDGE ( 'NONE', *, *, #25521, .F. ) ;
#34514=ORIENTED_EDGE ( 'NONE', *, *, #13374, .F. ) ;
#34516=ORIENTED_EDGE ( 'NONE', *, *, #30870, .T. ) ;
#34526=AXIS2_PLACEMENT_3D ( 'NONE', #13075, #35287, #25628 ) ;
#34527=CARTESIAN_POINT ( 'NONE',  ( -0.3000000000000000999, -3.318147336744930342, -0.6877918253319055264 ) ) ;
#34537=DIRECTION ( 'NONE',  ( 0.000000000000000000, -0.8438867430782091006, -0.5365213554527469286 ) ) ;
#34540=LINE ( 'NONE', #40294, #15971 ) ;
#34546=ORIENTED_EDGE ( 'NONE', *, *, #32500, .F. ) ;
#34565=DIRECTION ( 'NONE',  ( 1.000000000000000000, -0.000000000000000000, -0.000000000000000000 ) ) ;
#34569=EDGE_CURVE ( 'NONE', #27821, #10465, #8560, .T. ) ;
#34572=EDGE_LOOP ( 'NONE', ( #9905, #21419, #16639, #7530 ) ) ;
#34604=ORIENTED_EDGE ( 'NONE', *, *, #40550, .F. ) ;
#34614=DIRECTION ( 'NONE',  ( -1.000000000000000000, -0.000000000000000000, -0.000000000000000000 ) ) ;
#34622=VERTEX_POINT ( 'NONE', #11858 ) ;
#34629=EDGE_CURVE ( 'NONE', #14891, #37899, #2610, .T. ) ;
#34659=ADVANCED_FACE ( 'NONE', ( #28512 ), #774, .F. ) ;
#34661=ORIENTED_EDGE ( 'NONE', *, *, #24403, .F. ) ;
#34662=ORIENTED_EDGE ( 'NONE', *, *, #19556, .F. ) ;
#34672=CARTESIAN_POINT ( 'NONE',  ( -0.2399999999999999079, -4.074947978347777777, -0.4909924454747331413 ) ) ;
#34677=CONICAL_SURFACE ( 'NONE', #20220, 0.03999999999999933470, 1.047197551196598742 ) ;
#34682=CARTESIAN_POINT ( 'NONE',  ( -0.3000000000000000999, -2.416006048095809877, -1.059240699271965402 ) ) ;
#34684=DIRECTION ( 'NONE',  ( 0.000000000000000000, 2.731847993664262824E-15, -1.000000000000000000 ) ) ;
#34691=CARTESIAN_POINT ( 'NONE',  ( -0.2399999999999999079, -2.139295658456680904, -0.2024034539465678073 ) ) ;
#34698=ADVANCED_FACE ( 'NONE', ( #25020 ), #19266, .F. ) ;
#34699=EDGE_CURVE ( 'NONE', #27226, #6266, #9992, .T. ) ;
#34716=EDGE_LOOP ( 'NONE', ( #28138, #11336, #3941, #7359 ) ) ;
#34742=CARTESIAN_POINT ( 'NONE',  ( -0.2399999999999999079, -1.804235510932644004, -0.1501860188971498311 ) ) ;
#34748=ORIENTED_EDGE ( 'NONE', *, *, #32417, .F. ) ;
#34765=CARTESIAN_POINT ( 'NONE',  ( -0.3000000000000000999, -2.377368549242099949, -0.4802393080720198104 ) ) ;
#34766=CARTESIAN_POINT ( 'NONE',  ( -0.2399999999999999079, -4.289222312108804225, -0.5708809693675255259 ) ) ;
#34772=DIRECTION ( 'NONE',  ( 1.000000000000000000, 0.000000000000000000, 0.000000000000000000 ) ) ;
#34784=ORIENTED_EDGE ( 'NONE', *, *, #19556, .T. ) ;
#34786=ORIENTED_EDGE ( 'NONE', *, *, #25229, .F. ) ;
#34793=ORIENTED_EDGE ( 'NONE', *, *, #21604, .T. ) ;
#34796=VERTEX_POINT ( 'NONE', #7088 ) ;
#34809=VECTOR ( 'NONE', #30663, 39.37007874015748854 ) ;
#34812=ORIENTED_EDGE ( 'NONE', *, *, #30157, .T. ) ;
#34832=AXIS2_PLACEMENT_3D ( 'NONE', #34742, #6548, #6755 ) ;
#34847=FACE_OUTER_BOUND ( 'NONE', #10330, .T. ) ;
#34849=VERTEX_POINT ( 'NONE', #26855 ) ;
#34852=ORIENTED_EDGE ( 'NONE', *, *, #6065, .T. ) ;
#34877=AXIS2_PLACEMENT_3D ( 'NONE', #28035, #12382, #24937 ) ;
#34879=ADVANCED_FACE ( 'NONE', ( #30546 ), #39384, .F. ) ;
#34890=VERTEX_POINT ( 'NONE', #5224 ) ;
#34898=DIRECTION ( 'NONE',  ( -0.000000000000000000, 0.8159412518334725473, 0.5781348229923759519 ) ) ;
#34901=ORIENTED_EDGE ( 'NONE', *, *, #11681, .F. ) ;
#34916=ORIENTED_EDGE ( 'NONE', *, *, #10924, .F. ) ;
#34923=DIRECTION ( 'NONE',  ( 0.000000000000000000, 0.000000000000000000, -1.000000000000000000 ) ) ;
#34935=AXIS2_PLACEMENT_3D ( 'NONE', #34766, #6385, #28008 ) ;
#34948=VERTEX_POINT ( 'NONE', #13388 ) ;
#34954=DIRECTION ( 'NONE',  ( 0.000000000000000000, 3.414809992080318472E-15, -1.000000000000000000 ) ) ;
#35008=DIRECTION ( 'NONE',  ( 0.000000000000000000, 0.000000000000000000, -1.000000000000000000 ) ) ;
#35033=CIRCLE ( 'NONE', #39640, 0.1000000000000000194 ) ;
#35048=CARTESIAN_POINT ( 'NONE',  ( -0.3000000000000000999, -2.423474325126674156, -0.5576739111151496342 ) ) ;
#35050=VECTOR ( 'NONE', #36571, 39.37007874015748143 ) ;
#35054=PRODUCT ( 'Cage Hanger', 'Cage Hanger', '', ( #28455 ) ) ;
#35057=DIRECTION ( 'NONE',  ( 0.000000000000000000, 0.000000000000000000, -1.000000000000000000 ) ) ;
#35060=EDGE_CURVE ( 'NONE', #38034, #28698, #4328, .T. ) ;
#35068=AXIS2_PLACEMENT_3D ( 'NONE', #35634, #26802, #20834 ) ;
#35075=EDGE_CURVE ( 'NONE', #34796, #14911, #17079, .T. ) ;
#35076=LINE ( 'NONE', #6879, #14067 ) ;
#35078=EDGE_CURVE ( 'NONE', #23695, #4081, #36618, .T. ) ;
#35095=AXIS2_PLACEMENT_3D ( 'NONE', #18045, #30602, #2426 ) ;
#35098=VERTEX_POINT ( 'NONE', #13984 ) ;
#35119=EDGE_CURVE ( 'NONE', #22855, #7075, #31051, .T. ) ;
#35125=DIRECTION ( 'NONE',  ( 0.000000000000000000, 0.8159412518334726583, 0.5781348229923756188 ) ) ;
#35128=ORIENTED_EDGE ( 'NONE', *, *, #40550, .T. ) ;
#35139=DIRECTION ( 'NONE',  ( 0.000000000000000000, 0.000000000000000000, -1.000000000000000000 ) ) ;
#35148=CIRCLE ( 'NONE', #36461, 0.1000000000000000194 ) ;
#35150=ADVANCED_FACE ( 'NONE', ( #9226 ), #21606, .T. ) ;
#35152=DIRECTION ( 'NONE',  ( 0.000000000000000000, 0.000000000000000000, -1.000000000000000000 ) ) ;
#35154=DIRECTION ( 'NONE',  ( 1.000000000000000000, 0.000000000000000000, 0.000000000000000000 ) ) ;
#35166=ORIENTED_EDGE ( 'NONE', *, *, #20496, .T. ) ;
#35184=ORIENTED_EDGE ( 'NONE', *, *, #32376, .F. ) ;
#35192=CARTESIAN_POINT ( 'NONE',  ( -0.2399999999999999079, -4.074947978347777777, -0.4909924454747331413 ) ) ;
#35210=CONICAL_SURFACE ( 'NONE', #21424, 0.03999999999999930000, 1.047197551196598742 ) ;
#35224=DIRECTION ( 'NONE',  ( 1.000000000000000000, 0.000000000000000000, 0.000000000000000000 ) ) ;
#35226=ORIENTED_EDGE ( 'NONE', *, *, #40559, .T. ) ;
#35256=CARTESIAN_POINT ( 'NONE',  ( -0.3000000000000000999, -1.990692974992658737, -0.4647843861454829528 ) ) ;
#35257=DIRECTION ( 'NONE',  ( -1.000000000000000000, -0.000000000000000000, -0.000000000000000000 ) ) ;
#35266=ORIENTED_EDGE ( 'NONE', *, *, #23306, .F. ) ;
#35273=VECTOR ( 'NONE', #13710, 39.37007874015748143 ) ;
#35282=ORIENTED_EDGE ( 'NONE', *, *, #25741, .F. ) ;
#35286=FACE_OUTER_BOUND ( 'NONE', #902, .T. ) ;
#35287=DIRECTION ( 'NONE',  ( 1.000000000000000000, -0.000000000000000000, -0.000000000000000000 ) ) ;
#35301=EDGE_CURVE ( 'NONE', #25941, #23695, #37617, .T. ) ;
#35303=DIRECTION ( 'NONE',  ( -1.000000000000000000, -0.000000000000000000, -0.000000000000000000 ) ) ;
#35305=EDGE_CURVE ( 'NONE', #9001, #7421, #17878, .T. ) ;
#35307=EDGE_CURVE ( 'NONE', #9331, #6967, #20633, .T. ) ;
#35308=DIRECTION ( 'NONE',  ( -1.000000000000000000, -0.000000000000000000, -0.000000000000000000 ) ) ;
#35334=VECTOR ( 'NONE', #17099, 39.37007874015748854 ) ;
#35339=DIRECTION ( 'NONE',  ( 1.000000000000000000, 0.000000000000000000, 0.000000000000000000 ) ) ;
#35340=FACE_OUTER_BOUND ( 'NONE', #21870, .T. ) ;
#35366=DIRECTION ( 'NONE',  ( -1.000000000000000000, -0.000000000000000000, -0.000000000000000000 ) ) ;
#35384=DIRECTION ( 'NONE',  ( 0.000000000000000000, 0.000000000000000000, -1.000000000000000000 ) ) ;
#35413=CYLINDRICAL_SURFACE ( 'NONE', #29065, 0.1000000000000000194 ) ;
#35427=CARTESIAN_POINT ( 'NONE',  ( -0.2399999999999999079, -2.831259187443150971, -0.3041590760046470887 ) ) ;
#35438=EDGE_CURVE ( 'NONE', #18610, #11635, #13392, .T. ) ;
#35439=DIRECTION ( 'NONE',  ( -1.000000000000000000, -0.000000000000000000, -0.000000000000000000 ) ) ;
#35444=LINE ( 'NONE', #7244, #18022 ) ;
#35450=CARTESIAN_POINT ( 'NONE',  ( -0.2746410161513782033, -2.342996121808762044, -0.6842569225768811991 ) ) ;
#35472=DIRECTION ( 'NONE',  ( -1.000000000000000000, -0.000000000000000000, -0.000000000000000000 ) ) ;
#35482=FACE_OUTER_BOUND ( 'NONE', #13152, .T. ) ;
#35484=ORIENTED_EDGE ( 'NONE', *, *, #2355, .F. ) ;
#35485=CARTESIAN_POINT ( 'NONE',  ( -0.2399999999999999079, -3.647187793141847045, -0.4766722536777797115 ) ) ;
#35486=DIRECTION ( 'NONE',  ( 0.000000000000000000, 0.000000000000000000, -1.000000000000000000 ) ) ;
#35499=ORIENTED_EDGE ( 'NONE', *, *, #21048, .T. ) ;
#35501=CARTESIAN_POINT ( 'NONE',  ( -0.2399999999999999079, -4.098813193844367042, -0.6491724279539748954 ) ) ;
#35509=EDGE_LOOP ( 'NONE', ( #32258, #37428, #14398, #29188 ) ) ;
#35563=VERTEX_POINT ( 'NONE', #26065 ) ;
#35583=DIRECTION ( 'NONE',  ( 0.000000000000000000, 0.000000000000000000, -1.000000000000000000 ) ) ;
#35584=AXIS2_PLACEMENT_3D ( 'NONE', #16759, #13847, #32367 ) ;
#35586=DIRECTION ( 'NONE',  ( 1.000000000000000000, 0.000000000000000000, 0.000000000000000000 ) ) ;
#35588=VECTOR ( 'NONE', #25028, 39.37007874015748143 ) ;
#35593=EDGE_CURVE ( 'NONE', #1786, #9066, #35738, .T. ) ;
#35597=CARTESIAN_POINT ( 'NONE',  ( -0.2399999999999999079, -2.003129936916423048, -0.4197911229995844873 ) ) ;
#35600=CARTESIAN_POINT ( 'NONE',  ( -0.2746410161513779258, -3.705001275441084818, -0.3950781284944322458 ) ) ;
#35601=ORIENTED_EDGE ( 'NONE', *, *, #28356, .F. ) ;
#35602=CARTESIAN_POINT ( 'NONE',  ( -0.2746410161513782033, -2.289343986263487896, -0.7686455968847020204 ) ) ;
#35607=ORIENTED_EDGE ( 'NONE', *, *, #19748, .T. ) ;
#35612=AXIS2_PLACEMENT_3D ( 'NONE', #280, #12777, #25338 ) ;
#35623=DIRECTION ( 'NONE',  ( 0.000000000000000000, 0.000000000000000000, -1.000000000000000000 ) ) ;
#35634=CARTESIAN_POINT ( 'NONE',  ( -0.2399999999999999079, -2.511040369707300268, -0.4948468226404901804 ) ) ;
#35637=( NAMED_UNIT ( * ) SI_UNIT ( $, .STERADIAN. ) SOLID_ANGLE_UNIT ( ) );
#35644=VECTOR ( 'NONE', #22014, 39.37007874015748143 ) ;
#35647=ADVANCED_FACE ( 'NONE', ( #14178 ), #19974, .T. ) ;
#35649=ADVANCED_FACE ( 'NONE', ( #35984 ), #20562, .F. ) ;
#35653=VERTEX_POINT ( 'NONE', #24618 ) ;
#35657=ORIENTED_EDGE ( 'NONE', *, *, #38948, .F. ) ;
#35667=CARTESIAN_POINT ( 'NONE',  ( -0.2399999999999999079, -2.139295658456680904, -0.2024034539465678073 ) ) ;
#35668=ORIENTED_EDGE ( 'NONE', *, *, #3900, .T. ) ;
#35678=ORIENTED_EDGE ( 'NONE', *, *, #19848, .F. ) ;
#35681=VECTOR ( 'NONE', #33916, 39.37007874015748143 ) ;
#35685=EDGE_CURVE ( 'NONE', #39819, #10668, #15397, .T. ) ;
#35690=DIRECTION ( 'NONE',  ( 1.000000000000000000, 0.000000000000000000, 0.000000000000000000 ) ) ;
#35695=FACE_OUTER_BOUND ( 'NONE', #978, .T. ) ;
#35713=DIRECTION ( 'NONE',  ( 1.000000000000000000, -0.000000000000000000, -0.000000000000000000 ) ) ;
#35715=DIRECTION ( 'NONE',  ( -1.000000000000000000, 0.000000000000000000, 0.000000000000000000 ) ) ;
#35716=VERTEX_POINT ( 'NONE', #10898 ) ;
#35724=CIRCLE ( 'NONE', #33757, 0.1600000000000007527 ) ;
#35725=ORIENTED_EDGE ( 'NONE', *, *, #3126, .T. ) ;
#35732=VECTOR ( 'NONE', #2437, 39.37007874015749564 ) ;
#35738=CIRCLE ( 'NONE', #9453, 0.06250000000000001388 ) ;
#35753=FACE_OUTER_BOUND ( 'NONE', #25147, .T. ) ;
#35757=VERTEX_POINT ( 'NONE', #1449 ) ;
#35758=AXIS2_PLACEMENT_3D ( 'NONE', #11815, #27274, #33842 ) ;
#35759=ORIENTED_EDGE ( 'NONE', *, *, #39919, .T. ) ;
#35780=CARTESIAN_POINT ( 'NONE',  ( -0.2399999999999999079, -3.811657270145150989, -0.1642545796697100491 ) ) ;
#35785=FACE_OUTER_BOUND ( 'NONE', #14115, .T. ) ;
#35799=VECTOR ( 'NONE', #8818, 39.37007874015748143 ) ;
#35806=EDGE_CURVE ( 'NONE', #33666, #22635, #5513, .T. ) ;
#35810=LINE ( 'NONE', #16481, #32227 ) ;
#35811=EDGE_CURVE ( 'NONE', #14767, #28470, #23283, .T. ) ;
#35820=ORIENTED_EDGE ( 'NONE', *, *, #34392, .F. ) ;
#35824=FACE_OUTER_BOUND ( 'NONE', #2735, .T. ) ;
#35863=EDGE_CURVE ( 'NONE', #12532, #14064, #23256, .T. ) ;
#35873=DIRECTION ( 'NONE',  ( 0.000000000000000000, 0.000000000000000000, -1.000000000000000000 ) ) ;
#35878=CIRCLE ( 'NONE', #37851, 0.1946589359789743512 ) ;
#35885=EDGE_CURVE ( 'NONE', #15800, #32375, #22344, .T. ) ;
#35895=LINE ( 'NONE', #39375, #31108 ) ;
#35901=VECTOR ( 'NONE', #1824, 39.37007874015748143 ) ;
#35912=ADVANCED_FACE ( 'NONE', ( #19249 ), #3394, .F. ) ;
#35917=ORIENTED_EDGE ( 'NONE', *, *, #6354, .F. ) ;
#35939=DIRECTION ( 'NONE',  ( -0.4999999999999968359, 0.7308273574226419322, 0.4646411234949411884 ) ) ;
#35944=ADVANCED_FACE ( 'NONE', ( #19043 ), #37755, .F. ) ;
#35974=ORIENTED_EDGE ( 'NONE', *, *, #20545, .T. ) ;
#35984=FACE_OUTER_BOUND ( 'NONE', #32396, .T. ) ;
#35990=EDGE_CURVE ( 'NONE', #10078, #11732, #35076, .T. ) ;
#36015=ORIENTED_EDGE ( 'NONE', *, *, #10524, .T. ) ;
#36017=ORIENTED_EDGE ( 'NONE', *, *, #34401, .F. ) ;
#36023=CARTESIAN_POINT ( 'NONE',  ( -0.2746410161513782033, -2.183180860297908144, -0.9552969701112735690 ) ) ;
#36033=LINE ( 'NONE', #39514, #152 ) ;
#36055=ORIENTED_EDGE ( 'NONE', *, *, #32777, .T. ) ;
#36059=CARTESIAN_POINT ( 'NONE',  ( -0.2746410161513776482, -3.672249662662566472, -0.1880352225538197142 ) ) ;
#36067=ORIENTED_EDGE ( 'NONE', *, *, #21836, .F. ) ;
#36081=ORIENTED_EDGE ( 'NONE', *, *, #23626, .F. ) ;
#36101=CARTESIAN_POINT ( 'NONE',  ( -0.2746410161513779258, -3.985676108854518507, -0.7623095129438225426 ) ) ;
#36108=DIRECTION ( 'NONE',  ( 1.000000000000000000, -0.000000000000000000, -0.000000000000000000 ) ) ;
#36117=DIRECTION ( 'NONE',  ( -1.000000000000000000, -0.000000000000000000, -0.000000000000000000 ) ) ;
#36122=ORIENTED_EDGE ( 'NONE', *, *, #21854, .T. ) ;
#36123=VERTEX_POINT ( 'NONE', #16966 ) ;
#36152=EDGE_CURVE ( 'NONE', #354, #7026, #30314, .T. ) ;
#36153=ORIENTED_EDGE ( 'NONE', *, *, #5663, .F. ) ;
#36175=PLANE ( 'NONE',  #29035 ) ;
#36177=CARTESIAN_POINT ( 'NONE',  ( -0.2746410161513779258, -1.874946189051298617, -0.07947534077849530143 ) ) ;
#36185=FACE_OUTER_BOUND ( 'NONE', #20250, .T. ) ;
#36222=AXIS2_PLACEMENT_3D ( 'NONE', #12709, #38210, #37814 ) ;
#36226=AXIS2_PLACEMENT_3D ( 'NONE', #17749, #2130, #14665 ) ;
#36232=CARTESIAN_POINT ( 'NONE',  ( -0.2746410161513770931, -2.599675038826658735, -0.8213992999509311943 ) ) ;
#36247=AXIS2_PLACEMENT_3D ( 'NONE', #26154, #32100, #19959 ) ;
#36258=ORIENTED_EDGE ( 'NONE', *, *, #37614, .F. ) ;
#36270=CARTESIAN_POINT ( 'NONE',  ( -0.3000000000000000999, -3.970782550070895311, -0.6634248229925526763 ) ) ;
#36276=DIRECTION ( 'NONE',  ( 1.000000000000000000, -0.000000000000000000, -0.000000000000000000 ) ) ;
#36312=ADVANCED_FACE ( 'NONE', ( #14893 ), #36448, .F. ) ;
#36313=FACE_OUTER_BOUND ( 'NONE', #34233, .T. ) ;
#36327=DIRECTION ( 'NONE',  ( 1.000000000000000000, 0.000000000000000000, 0.000000000000000000 ) ) ;
#36354=DIRECTION ( 'NONE',  ( -1.000000000000000000, -0.000000000000000000, -0.000000000000000000 ) ) ;
#36358=FACE_OUTER_BOUND ( 'NONE', #3086, .T. ) ;
#36404=CIRCLE ( 'NONE', #39690, 0.6115209409081865388 ) ;
#36411=CARTESIAN_POINT ( 'NONE',  ( -0.2399999999999999079, -2.768941938641841904, -0.5551618215276492574 ) ) ;
#36420=DIRECTION ( 'NONE',  ( 0.4261641068392654774, -0.9046458721742397513, 0.000000000000000000 ) ) ;
#36422=ORIENTED_EDGE ( 'NONE', *, *, #10233, .T. ) ;
#36426=ORIENTED_EDGE ( 'NONE', *, *, #7490, .F. ) ;
#36433=CARTESIAN_POINT ( 'NONE',  ( -0.2746410161513770931, -3.217981293616048344, -0.2530108926800491709 ) ) ;
#36440=CIRCLE ( 'NONE', #14118, 0.4615209409081865166 ) ;
#36448=CONICAL_SURFACE ( 'NONE', #38407, 0.1600000000000016964, 1.047197551196601406 ) ;
#36461=AXIS2_PLACEMENT_3D ( 'NONE', #30673, #33963, #39923 ) ;
#36462=CONICAL_SURFACE ( 'NONE', #8859, 0.03999999999999950817, 1.047197551196597409 ) ;
#36484=CARTESIAN_POINT ( 'NONE',  ( -0.2399999999999999079, -3.701811653776600597, -0.3192834175180689904 ) ) ;
#36493=ORIENTED_EDGE ( 'NONE', *, *, #25626, .F. ) ;
#36498=VECTOR ( 'NONE', #2411, 39.37007874015748143 ) ;
#36543=VERTEX_POINT ( 'NONE', #7040 ) ;
#36553=AXIS2_PLACEMENT_3D ( 'NONE', #32239, #16626, #1414 ) ;
#36555=EDGE_CURVE ( 'NONE', #38935, #17501, #18132, .T. ) ;
#36571=DIRECTION ( 'NONE',  ( -1.000000000000000000, -0.000000000000000000, -0.000000000000000000 ) ) ;
#36573=VERTEX_POINT ( 'NONE', #30257 ) ;
#36575=EDGE_CURVE ( 'NONE', #14323, #33695, #39324, .T. ) ;
#36582=VERTEX_POINT ( 'NONE', #11144 ) ;
#36594=ORIENTED_EDGE ( 'NONE', *, *, #31662, .F. ) ;
#36618=LINE ( 'NONE', #10918, #31107 ) ;
#36631=ORIENTED_EDGE ( 'NONE', *, *, #20793, .F. ) ;
#36635=DIRECTION ( 'NONE',  ( 0.000000000000000000, 0.000000000000000000, -1.000000000000000000 ) ) ;
#36666=ORIENTED_EDGE ( 'NONE', *, *, #6399, .F. ) ;
#36694=ORIENTED_EDGE ( 'NONE', *, *, #2660, .T. ) ;
#36698=CARTESIAN_POINT ( 'NONE',  ( -0.2399999999999999079, -2.183180860297908144, -1.015296970111275510 ) ) ;
#36701=PLANE ( 'NONE',  #26673 ) ;
#36751=CARTESIAN_POINT ( 'NONE',  ( -0.3000000000000000999, -4.394818335734379744, -0.8816972205720928768 ) ) ;
#36756=FACE_OUTER_BOUND ( 'NONE', #17623, .T. ) ;
#36759=LINE ( 'NONE', #29790, #7281 ) ;
#36803=AXIS2_PLACEMENT_3D ( 'NONE', #40255, #5487, #24653 ) ;
#36812=ORIENTED_EDGE ( 'NONE', *, *, #15748, .F. ) ;
#36814=DIRECTION ( 'NONE',  ( 0.000000000000000000, 0.7071067811865474617, 0.7071067811865474617 ) ) ;
#36816=ORIENTED_EDGE ( 'NONE', *, *, #33303, .F. ) ;
#36837=FACE_BOUND ( 'NONE', #7822, .T. ) ;
#36854=VERTEX_POINT ( 'NONE', #33101 ) ;
#36863=AXIS2_PLACEMENT_3D ( 'NONE', #3932, #32129, #2779 ) ;
#36876=AXIS2_PLACEMENT_3D ( 'NONE', #26168, #31716, #3744 ) ;
#36877=EDGE_CURVE ( 'NONE', #19496, #37899, #27147, .T. ) ;
#36894=EDGE_CURVE ( 'NONE', #17501, #34890, #40498, .T. ) ;
#36903=CIRCLE ( 'NONE', #4705, 0.1600000000000000588 ) ;
#36931=CARTESIAN_POINT ( 'NONE',  ( -0.2399999999999999079, -3.285933380171606188, -0.6294744526254049122 ) ) ;
#36946=DIRECTION ( 'NONE',  ( -0.4999999999999985567, 0.2711473017028560029, 0.8224835200654551093 ) ) ;
#36959=AXIS2_PLACEMENT_3D ( 'NONE', #23879, #14381, #5311 ) ;
#36961=ORIENTED_EDGE ( 'NONE', *, *, #35119, .F. ) ;
#36967=VERTEX_POINT ( 'NONE', #6734 ) ;
#36968=DIRECTION ( 'NONE',  ( 0.000000000000000000, 0.000000000000000000, -1.000000000000000000 ) ) ;
#36969=CONICAL_SURFACE ( 'NONE', #16664, 0.1600000000000000588, 1.047197551196602738 ) ;
#36970=DIRECTION ( 'NONE',  ( -1.000000000000000000, -0.000000000000000000, -0.000000000000000000 ) ) ;
#36975=VERTEX_POINT ( 'NONE', #38618 ) ;
#36988=ORIENTED_EDGE ( 'NONE', *, *, #30750, .T. ) ;
#37002=AXIS2_PLACEMENT_3D ( 'NONE', #968, #7271, #31399 ) ;
#37017=AXIS2_PLACEMENT_3D ( 'NONE', #3685, #2870, #15420 ) ;
#37020=DIRECTION ( 'NONE',  ( 0.000000000000000000, 0.000000000000000000, -1.000000000000000000 ) ) ;
#37043=CARTESIAN_POINT ( 'NONE',  ( -0.3000000000000000999, -3.838583118162426810, -0.3058907208964237734 ) ) ;
#37056=ADVANCED_FACE ( 'NONE', ( #35340 ), #22206, .T. ) ;
#37062=AXIS2_PLACEMENT_3D ( 'NONE', #40594, #12413, #34017 ) ;
#37065=LINE ( 'NONE', #31317, #8323 ) ;
#37084=ADVANCED_FACE ( 'NONE', ( #29161 ), #9519, .F. ) ;
#37102=ADVANCED_FACE ( 'NONE', ( #39425 ), #18751, .T. ) ;
#37111=CIRCLE ( 'NONE', #6883, 0.1946589359789743512 ) ;
#37143=VECTOR ( 'NONE', #32840, 39.37007874015748143 ) ;
#37148=CARTESIAN_POINT ( 'NONE',  ( -0.2399999999999999079, -3.941790907013290823, -0.4709369376873030477 ) ) ;
#37151=CARTESIAN_POINT ( 'NONE',  ( -0.3000000000000000999, -3.941790907013290823, -0.2762780017083287243 ) ) ;
#37160=LINE ( 'NONE', #21122, #38920 ) ;
#37201=EDGE_LOOP ( 'NONE', ( #37232, #15180, #25472, #39800 ) ) ;
#37215=CARTESIAN_POINT ( 'NONE',  ( -0.2399999999999999079, -4.385325017590463226, -0.5985264029706663935 ) ) ;
#37232=ORIENTED_EDGE ( 'NONE', *, *, #35885, .T. ) ;
#37236=LINE ( 'NONE', #20809, #34809 ) ;
#37250=CARTESIAN_POINT ( 'NONE',  ( -0.2399999999999999079, -3.417177400252447317, -1.296093996387527758 ) ) ;
#37257=CIRCLE ( 'NONE', #1809, 0.6115209409081865388 ) ;
#37261=CARTESIAN_POINT ( 'NONE',  ( -0.2399999999999999079, -3.647187793141847045, -0.4766722536777797115 ) ) ;
#37288=EDGE_CURVE ( 'NONE', #19496, #28467, #5464, .T. ) ;
#37325=ORIENTED_EDGE ( 'NONE', *, *, #4995, .T. ) ;
#37329=CARTESIAN_POINT ( 'NONE',  ( -0.2746410161513770931, -3.253611865733782693, -0.3464478357516359575 ) ) ;
#37342=CARTESIAN_POINT ( 'NONE',  ( -0.2399999999999999079, -3.931184305295492898, -0.4815435394051006956 ) ) ;
#37350=EDGE_LOOP ( 'NONE', ( #34514, #5274, #5034, #33959 ) ) ;
#37360=CARTESIAN_POINT ( 'NONE',  ( -0.3000000000000000999, -3.941790907013290823, 0.1405840032208834911 ) ) ;
#37364=FACE_OUTER_BOUND ( 'NONE', #7690, .T. ) ;
#37371=ORIENTED_EDGE ( 'NONE', *, *, #7490, .T. ) ;
#37374=DIRECTION ( 'NONE',  ( -0.5000000000000012212, -0.7066258520834619583, -0.5006794435238177687 ) ) ;
#37399=DIRECTION ( 'NONE',  ( 0.4379975771764363368, 0.000000000000000000, 0.8989761522907998570 ) ) ;
#37423=FACE_OUTER_BOUND ( 'NONE', #24756, .T. ) ;
#37428=ORIENTED_EDGE ( 'NONE', *, *, #11878, .F. ) ;
#37442=CARTESIAN_POINT ( 'NONE',  ( -0.2399999999999999079, -2.004945370031237850, -0.3367537423720109446 ) ) ;
#37447=DIRECTION ( 'NONE',  ( 0.000000000000000000, 0.000000000000000000, 1.000000000000000000 ) ) ;
#37460=LINE ( 'NONE', #9277, #12669 ) ;
#37472=ORIENTED_EDGE ( 'NONE', *, *, #7614, .T. ) ;
#37478=CARTESIAN_POINT ( 'NONE',  ( -0.3000000000000000999, -3.667123564397057667, -0.3682398926280779361 ) ) ;
#37518=CARTESIAN_POINT ( 'NONE',  ( -0.2399999999999999079, -3.807157481699992907, -0.4735579732456337565 ) ) ;
#37519=CARTESIAN_POINT ( 'NONE',  ( -0.2399999999999999079, -3.723902497147952406, 0.1004495357399106253 ) ) ;
#37522=EDGE_LOOP ( 'NONE', ( #15631, #17093, #7159, #39992 ) ) ;
#37523=CONICAL_SURFACE ( 'NONE', #19802, 0.1946589359789743512, 1.047197551196599186 ) ;
#37528=EDGE_CURVE ( 'NONE', #19589, #11583, #2095, .T. ) ;
#37534=EDGE_LOOP ( 'NONE', ( #4019, #27434, #18680, #26135 ) ) ;
#37542=DIRECTION ( 'NONE',  ( 1.000000000000000000, 0.000000000000000000, 0.000000000000000000 ) ) ;
#37544=VECTOR ( 'NONE', #23074, 39.37007874015748143 ) ;
#37601=CIRCLE ( 'NONE', #11971, 0.06250000000000001388 ) ;
#37606=FACE_OUTER_BOUND ( 'NONE', #31563, .T. ) ;
#37614=EDGE_CURVE ( 'NONE', #4836, #18572, #20724, .T. ) ;
#37617=LINE ( 'NONE', #40087, #39638 ) ;
#37624=CARTESIAN_POINT ( 'NONE',  ( -0.2746410161513776482, -3.758594918004649621, -0.06617323996463192470 ) ) ;
#37631=ORIENTED_EDGE ( 'NONE', *, *, #36877, .F. ) ;
#37636=AXIS2_PLACEMENT_3D ( 'NONE', #27919, #15968, #28515 ) ;
#37639=EDGE_CURVE ( 'NONE', #34948, #33422, #27806, .T. ) ;
#37644=ADVANCED_FACE ( 'NONE', ( #40342 ), #37878, .F. ) ;
#37662=DIRECTION ( 'NONE',  ( 0.000000000000000000, 0.5781348229923761739, -0.8159412518334723252 ) ) ;
#37663=CARTESIAN_POINT ( 'NONE',  ( -0.3000000000000000999, -4.320736256378554963, -0.8145269479932405465 ) ) ;
#37669=AXIS2_PLACEMENT_3D ( 'NONE', #19526, #18920, #38029 ) ;
#37674=EDGE_CURVE ( 'NONE', #38708, #591, #8896, .T. ) ;
#37689=DIRECTION ( 'NONE',  ( 0.000000000000000000, 0.000000000000000000, -1.000000000000000000 ) ) ;
#37701=EDGE_LOOP ( 'NONE', ( #36961, #18324, #38463, #28042 ) ) ;
#37711=CARTESIAN_POINT ( 'NONE',  ( -0.2399999999999999079, -4.120026397279962005, -0.6279592245183788224 ) ) ;
#37733=ORIENTED_EDGE ( 'NONE', *, *, #36152, .F. ) ;
#37735=DIRECTION ( 'NONE',  ( 0.000000000000000000, 0.000000000000000000, -1.000000000000000000 ) ) ;
#37746=ORIENTED_EDGE ( 'NONE', *, *, #21732, .T. ) ;
#37753=AXIS2_PLACEMENT_3D ( 'NONE', #5391, #24159, #21474 ) ;
#37755=PLANE ( 'NONE',  #29841 ) ;
#37763=DIRECTION ( 'NONE',  ( 1.000000000000000000, -0.000000000000000000, -0.000000000000000000 ) ) ;
#37812=CARTESIAN_POINT ( 'NONE',  ( -0.2746410161513770931, -3.156018320128275878, -0.4841849112664152743 ) ) ;
#37814=DIRECTION ( 'NONE',  ( 0.000000000000000000, -0.9246857012436752177, 0.3807313408632029827 ) ) ;
#37818=EDGE_CURVE ( 'NONE', #16911, #38708, #40444, .T. ) ;
#37821=VECTOR ( 'NONE', #30176, 39.37007874015748143 ) ;
#37831=DIRECTION ( 'NONE',  ( 0.000000000000000000, 0.5365213554527469286, -0.8438867430782091006 ) ) ;
#37839=CYLINDRICAL_SURFACE ( 'NONE', #37017, 0.1000000000000000194 ) ;
#37840=LINE ( 'NONE', #38033, #15205 ) ;
#37843=FACE_OUTER_BOUND ( 'NONE', #17052, .T. ) ;
#37851=AXIS2_PLACEMENT_3D ( 'NONE', #39571, #14472, #1775 ) ;
#37877=LINE ( 'NONE', #6577, #8644 ) ;
#37878=CYLINDRICAL_SURFACE ( 'NONE', #38477, 0.1000000000000000194 ) ;
#37891=LINE ( 'NONE', #35600, #37544 ) ;
#37899=VERTEX_POINT ( 'NONE', #16277 ) ;
#37900=CARTESIAN_POINT ( 'NONE',  ( -0.2399999999999999079, -3.196602950345407645, -0.1969487268370971322 ) ) ;
#37908=EDGE_CURVE ( 'NONE', #591, #27450, #30582, .T. ) ;
#37909=CARTESIAN_POINT ( 'NONE',  ( -0.3000000000000000999, -3.985676108854518507, -0.7623095129438225426 ) ) ;
#37913=ORIENTED_EDGE ( 'NONE', *, *, #30356, .F. ) ;
#37914=EDGE_CURVE ( 'NONE', #11635, #18456, #32495, .T. ) ;
#37918=DIRECTION ( 'NONE',  ( -0.4999999999999948375, 0.7066258520834660661, 0.5006794435238187679 ) ) ;
#37920=CARTESIAN_POINT ( 'NONE',  ( -0.3000000000000000999, -4.218511633990150500, -0.6415916474861803609 ) ) ;
#37921=ADVANCED_FACE ( 'NONE', ( #22669 ), #2334, .F. ) ;
#37927=DIRECTION ( 'NONE',  ( 0.000000000000000000, 0.000000000000000000, -1.000000000000000000 ) ) ;
#37936=PLANE ( 'NONE',  #27229 ) ;
#37943=ORIENTED_EDGE ( 'NONE', *, *, #34699, .T. ) ;
#37947=LINE ( 'NONE', #32727, #3785 ) ;
#37980=ORIENTED_EDGE ( 'NONE', *, *, #34629, .T. ) ;
#37985=ADVANCED_FACE ( 'NONE', ( #20577 ), #11304, .F. ) ;
#37990=DIRECTION ( 'NONE',  ( 1.000000000000000000, 0.000000000000000000, 0.000000000000000000 ) ) ;
#38000=ORIENTED_EDGE ( 'NONE', *, *, #37639, .F. ) ;
#38003=CARTESIAN_POINT ( 'NONE',  ( -0.2746410161513776482, -3.941790907013290823, -0.4709369376873030477 ) ) ;
#38009=CARTESIAN_POINT ( 'NONE',  ( -0.2399999999999999079, -3.156018320128275878, -0.4841849112664152743 ) ) ;
#38014=FACE_BOUND ( 'NONE', #14988, .T. ) ;
#38018=DIRECTION ( 'NONE',  ( 1.000000000000000000, -0.000000000000000000, -0.000000000000000000 ) ) ;
#38029=DIRECTION ( 'NONE',  ( 0.000000000000000000, 0.000000000000000000, -1.000000000000000000 ) ) ;
#38033=CARTESIAN_POINT ( 'NONE',  ( -0.2746410161513776482, -3.753843787845913216, -0.2458487048530572650 ) ) ;
#38034=VERTEX_POINT ( 'NONE', #11712 ) ;
#38037=ORIENTED_EDGE ( 'NONE', *, *, #13558, .F. ) ;
#38038=CARTESIAN_POINT ( 'NONE',  ( -0.2399999999999999079, -1.730153431576819001, -0.08301574631829765349 ) ) ;
#38076=ADVANCED_FACE ( 'NONE', ( #23664 ), #6249, .F. ) ;
#38083=EDGE_CURVE ( 'NONE', #28470, #12691, #3011, .T. ) ;
#38088=EDGE_LOOP ( 'NONE', ( #28709, #18461, #9567, #8293 ) ) ;
#38089=CARTESIAN_POINT ( 'NONE',  ( -0.2399999999999999079, -2.289343986263487896, -0.7686455968847020204 ) ) ;
#38099=EDGE_CURVE ( 'NONE', #4081, #26629, #11106, .T. ) ;
#38110=( NAMED_UNIT ( * ) PLANE_ANGLE_UNIT ( ) SI_UNIT ( $, .RADIAN. ) );
#38125=FACE_OUTER_BOUND ( 'NONE', #17291, .T. ) ;
#38128=EDGE_CURVE ( 'NONE', #20955, #26127, #29286, .T. ) ;
#38138=DIRECTION ( 'NONE',  ( 1.000000000000000000, -0.000000000000000000, -0.000000000000000000 ) ) ;
#38144=ORIENTED_EDGE ( 'NONE', *, *, #17759, .F. ) ;
#38159=CONICAL_SURFACE ( 'NONE', #33564, 0.1600000000000006140, 1.047197551196598297 ) ;
#38165=CIRCLE ( 'NONE', #20440, 0.4615209409081865166 ) ;
#38167=DIRECTION ( 'NONE',  ( -1.000000000000000000, -0.000000000000000000, -0.000000000000000000 ) ) ;
#38173=CARTESIAN_POINT ( 'NONE',  ( -0.2746410161513782033, -2.183180860297908144, -0.4937760292030871079 ) ) ;
#38185=VECTOR ( 'NONE', #26468, 39.37007874015748854 ) ;
#38207=ORIENTED_EDGE ( 'NONE', *, *, #2257, .T. ) ;
#38210=DIRECTION ( 'NONE',  ( -0.000000000000000000, 0.3807313408632030383, 0.9246857012436753287 ) ) ;
#38216=LINE ( 'NONE', #3861, #863 ) ;
#38232=ORIENTED_EDGE ( 'NONE', *, *, #5740, .T. ) ;
#38234=CARTESIAN_POINT ( 'NONE',  ( -0.2399999999999999079, -2.511040369707300268, -0.4948468226404901804 ) ) ;
#38240=ORIENTED_EDGE ( 'NONE', *, *, #13288, .T. ) ;
#38244=CARTESIAN_POINT ( 'NONE',  ( -0.2746410161513779258, -3.609310082097819894, -0.4498340178114252352 ) ) ;
#38255=VECTOR ( 'NONE', #16270, 39.37007874015748854 ) ;
#38256=VECTOR ( 'NONE', #15907, 39.37007874015748143 ) ;
#38259=AXIS2_PLACEMENT_3D ( 'NONE', #32167, #31972, #16150 ) ;
#38273=PLANE ( 'NONE',  #14257 ) ;
#38281=DIRECTION ( 'NONE',  ( -0.000000000000000000, -0.7071067811865474617, -0.7071067811865474617 ) ) ;
#38284=ORIENTED_EDGE ( 'NONE', *, *, #38099, .T. ) ;
#38286=ORIENTED_EDGE ( 'NONE', *, *, #26778, .T. ) ;
#38287=DIRECTION ( 'NONE',  ( 0.000000000000000000, 0.000000000000000000, 1.000000000000000000 ) ) ;
#38321=DIRECTION ( 'NONE',  ( 0.000000000000000000, 0.000000000000000000, 1.000000000000000000 ) ) ;
#38350=ORIENTED_EDGE ( 'NONE', *, *, #39190, .T. ) ;
#38356=LINE ( 'NONE', #3998, #21219 ) ;
#38368=ORIENTED_EDGE ( 'NONE', *, *, #3141, .F. ) ;
#38379=LINE ( 'NONE', #22783, #16710 ) ;
#38392=AXIS2_PLACEMENT_3D ( 'NONE', #3847, #16221, #6524 ) ;
#38406=VERTEX_POINT ( 'NONE', #26109 ) ;
#38407=AXIS2_PLACEMENT_3D ( 'NONE', #27642, #2351, #27451 ) ;
#38420=DIRECTION ( 'NONE',  ( 0.000000000000000000, 0.000000000000000000, -1.000000000000000000 ) ) ;
#38424=AXIS2_PLACEMENT_3D ( 'NONE', #38969, #20458, #39186 ) ;
#38425=DIRECTION ( 'NONE',  ( 1.000000000000000000, 0.000000000000000000, 0.000000000000000000 ) ) ;
#38440=VECTOR ( 'NONE', #14632, 39.37007874015748854 ) ;
#38450=ORIENTED_EDGE ( 'NONE', *, *, #35863, .T. ) ;
#38457=DIRECTION ( 'NONE',  ( -1.000000000000000000, -0.000000000000000000, -0.000000000000000000 ) ) ;
#38461=VECTOR ( 'NONE', #24260, 39.37007874015748143 ) ;
#38463=ORIENTED_EDGE ( 'NONE', *, *, #36894, .T. ) ;
#38474=ADVANCED_FACE ( 'NONE', ( #13328 ), #26047, .F. ) ;
#38477=AXIS2_PLACEMENT_3D ( 'NONE', #37261, #3300, #21846 ) ;
#38480=CARTESIAN_POINT ( 'NONE',  ( -0.2746410161513770931, -2.891403747035983240, -0.7012825271972917829 ) ) ;
#38530=LINE ( 'NONE', #10361, #28719 ) ;
#38531=FACE_OUTER_BOUND ( 'NONE', #35509, .T. ) ;
#38554=ADVANCED_FACE ( 'NONE', ( #26491 ), #5629, .F. ) ;
#38582=DIRECTION ( 'NONE',  ( 0.000000000000000000, -0.9246857012436752177, 0.3807313408632033713 ) ) ;
#38590=CARTESIAN_POINT ( 'NONE',  ( -0.2399999999999999079, -4.120026397279962005, -0.6279592245183788224 ) ) ;
#38618=CARTESIAN_POINT ( 'NONE',  ( -0.2746410161513782033, -1.990692974992658737, -0.4647843861454829528 ) ) ;
#38635=AXIS2_PLACEMENT_3D ( 'NONE', #39460, #2247, #14170 ) ;
#38637=VERTEX_POINT ( 'NONE', #31999 ) ;
#38652=ORIENTED_EDGE ( 'NONE', *, *, #33366, .T. ) ;
#38658=ORIENTED_EDGE ( 'NONE', *, *, #34387, .F. ) ;
#38662=DIRECTION ( 'NONE',  ( -0.8660254037844390407, 0.3535533905932734533, -0.3535533905932734533 ) ) ;
#38692=ORIENTED_EDGE ( 'NONE', *, *, #31760, .T. ) ;
#38693=EDGE_CURVE ( 'NONE', #28467, #478, #25364, .T. ) ;
#38698=LINE ( 'NONE', #13799, #6164 ) ;
#38700=DIRECTION ( 'NONE',  ( 1.000000000000000000, 0.000000000000000000, 0.000000000000000000 ) ) ;
#38703=ORIENTED_EDGE ( 'NONE', *, *, #24920, .T. ) ;
#38708=VERTEX_POINT ( 'NONE', #974 ) ;
#38732=DIRECTION ( 'NONE',  ( 0.4999999999999975575, 0.8322738431953016214, 0.2394164779895586459 ) ) ;
#38761=CYLINDRICAL_SURFACE ( 'NONE', #28465, 0.1000000000000000194 ) ;
#38767=AXIS2_PLACEMENT_3D ( 'NONE', #23494, #20807, #11319 ) ;
#38780=DIRECTION ( 'NONE',  ( -0.000000000000000000, -0.5365213554527469286, 0.8438867430782088785 ) ) ;
#38785=ORIENTED_EDGE ( 'NONE', *, *, #16782, .T. ) ;
#38787=ORIENTED_EDGE ( 'NONE', *, *, #23159, .T. ) ;
#38793=AXIS2_PLACEMENT_3D ( 'NONE', #13462, #10374, #35873 ) ;
#38796=CARTESIAN_POINT ( 'NONE',  ( -0.2399999999999999079, -3.253611865733782693, -0.3464478357516359575 ) ) ;
#38798=ORIENTED_EDGE ( 'NONE', *, *, #36152, .T. ) ;
#38820=CARTESIAN_POINT ( 'NONE',  ( -0.2399999999999999079, -2.183180860297908144, -0.4937760292030871079 ) ) ;
#38829=ORIENTED_EDGE ( 'NONE', *, *, #17306, .F. ) ;
#38833=ORIENTED_EDGE ( 'NONE', *, *, #35060, .F. ) ;
#38899=DIRECTION ( 'NONE',  ( 0.000000000000000000, 0.000000000000000000, 1.000000000000000000 ) ) ;
#38909=DIRECTION ( 'NONE',  ( 1.000000000000000000, -0.000000000000000000, -0.000000000000000000 ) ) ;
#38919=( LENGTH_UNIT ( ) NAMED_UNIT ( * ) SI_UNIT ( $, .METRE. ) );
#38920=VECTOR ( 'NONE', #18025, 39.37007874015748854 ) ;
#38935=VERTEX_POINT ( 'NONE', #7707 ) ;
#38946=EDGE_LOOP ( 'NONE', ( #4296, #5186, #39182, #7062 ) ) ;
#38948=EDGE_CURVE ( 'NONE', #15927, #38637, #480, .T. ) ;
#38965=VERTEX_POINT ( 'NONE', #40184 ) ;
#38969=CARTESIAN_POINT ( 'NONE',  ( -0.2746410161513779258, -3.253295730098268113, -0.6063490597057096254 ) ) ;
#39003=ORIENTED_EDGE ( 'NONE', *, *, #8114, .F. ) ;
#39005=ORIENTED_EDGE ( 'NONE', *, *, #9431, .F. ) ;
#39012=CARTESIAN_POINT ( 'NONE',  ( -0.2399999999999999079, -3.647187793141847045, -0.4766722536777797115 ) ) ;
#39014=ORIENTED_EDGE ( 'NONE', *, *, #9676, .F. ) ;
#39017=AXIS2_PLACEMENT_3D ( 'NONE', #26453, #14099, #29343 ) ;
#39042=VECTOR ( 'NONE', #30423, 39.37007874015748143 ) ;
#39043=ORIENTED_EDGE ( 'NONE', *, *, #37914, .T. ) ;
#39059=DIRECTION ( 'NONE',  ( -1.000000000000000000, -0.000000000000000000, -0.000000000000000000 ) ) ;
#39103=ORIENTED_EDGE ( 'NONE', *, *, #26822, .T. ) ;
#39117=PRODUCT_DEFINITION_FORMATION_WITH_SPECIFIED_SOURCE ( 'ANY', '', #35054, .NOT_KNOWN. ) ;
#39133=CARTESIAN_POINT ( 'NONE',  ( -0.2399999999999999079, -3.068736697824639759, 0.08412833800243627036 ) ) ;
#39135=DIRECTION ( 'NONE',  ( -0.4261641068392685860, 0.000000000000000000, 0.9046458721742383080 ) ) ;
#39142=VECTOR ( 'NONE', #19491, 39.37007874015748143 ) ;
#39144=CARTESIAN_POINT ( 'NONE',  ( -0.2746410161513779258, -1.804235510932644004, -0.05018601889714981862 ) ) ;
#39159=CARTESIAN_POINT ( 'NONE',  ( -0.2399999999999999079, -3.941790907013290823, -0.4709369376873030477 ) ) ;
#39167=DIRECTION ( 'NONE',  ( 0.000000000000000000, 0.000000000000000000, -1.000000000000000000 ) ) ;
#39173=CIRCLE ( 'NONE', #3061, 0.03999999999999950817 ) ;
#39182=ORIENTED_EDGE ( 'NONE', *, *, #32557, .F. ) ;
#39186=DIRECTION ( 'NONE',  ( 0.000000000000000000, 0.000000000000000000, -1.000000000000000000 ) ) ;
#39190=EDGE_CURVE ( 'NONE', #12319, #22735, #22113, .T. ) ;
#39191=CYLINDRICAL_SURFACE ( 'NONE', #20529, 0.1946589359789743512 ) ;
#39200=PLANE ( 'NONE',  #889 ) ;
#39203=ORIENTED_EDGE ( 'NONE', *, *, #9000, .F. ) ;
#39205=DIRECTION ( 'NONE',  ( 1.000000000000000000, 0.000000000000000000, 0.000000000000000000 ) ) ;
#39223=DIRECTION ( 'NONE',  ( 0.000000000000000000, 0.000000000000000000, -1.000000000000000000 ) ) ;
#39271=ORIENTED_EDGE ( 'NONE', *, *, #10924, .T. ) ;
#39272=DIRECTION ( 'NONE',  ( 0.000000000000000000, 0.000000000000000000, -1.000000000000000000 ) ) ;
#39324=LINE ( 'NONE', #39133, #33159 ) ;
#39336=EDGE_CURVE ( 'NONE', #24285, #3165, #33268, .T. ) ;
#39375=CARTESIAN_POINT ( 'NONE',  ( -0.2399999999999999079, -2.183180860297908144, -0.3591170932241134484 ) ) ;
#39378=DIRECTION ( 'NONE',  ( 0.000000000000000000, 0.000000000000000000, 1.000000000000000000 ) ) ;
#39384=CYLINDRICAL_SURFACE ( 'NONE', #2219, 0.1000000000000000194 ) ;
#39390=ORIENTED_EDGE ( 'NONE', *, *, #31822, .T. ) ;
#39399=LINE ( 'NONE', #23591, #32937 ) ;
#39403=CARTESIAN_POINT ( 'NONE',  ( -0.2399999999999999079, -3.681106669851795132, -0.07175300799092947102 ) ) ;
#39406=ORIENTED_EDGE ( 'NONE', *, *, #36575, .T. ) ;
#39407=ADVANCED_FACE ( 'NONE', ( #25110 ), #18742, .T. ) ;
#39416=ORIENTED_EDGE ( 'NONE', *, *, #22110, .F. ) ;
#39425=FACE_OUTER_BOUND ( 'NONE', #11540, .T. ) ;
#39434=DIRECTION ( 'NONE',  ( 1.000000000000000000, 0.000000000000000000, 0.000000000000000000 ) ) ;
#39436=FACE_OUTER_BOUND ( 'NONE', #23774, .T. ) ;
#39443=ORIENTED_EDGE ( 'NONE', *, *, #33563, .F. ) ;
#39460=CARTESIAN_POINT ( 'NONE',  ( -0.2399999999999999079, -3.849534981189179028, -0.1910928155360645808 ) ) ;
#39470=CARTESIAN_POINT ( 'NONE',  ( -0.2399999999999999079, -2.183180860297908144, -0.4937760292030871079 ) ) ;
#39487=ORIENTED_EDGE ( 'NONE', *, *, #5444, .T. ) ;
#39498=DIRECTION ( 'NONE',  ( 0.000000000000000000, -0.7071067811865474617, -0.7071067811865475727 ) ) ;
#39514=CARTESIAN_POINT ( 'NONE',  ( -0.2746410161513782033, -2.253314830856113726, -0.6753616220517687507 ) ) ;
#39546=DIRECTION ( 'NONE',  ( 0.000000000000000000, 0.000000000000000000, -1.000000000000000000 ) ) ;
#39551=EDGE_CURVE ( 'NONE', #35716, #4635, #30666, .T. ) ;
#39553=EDGE_CURVE ( 'NONE', #9411, #25380, #28754, .T. ) ;
#39571=CARTESIAN_POINT ( 'NONE',  ( -0.2746410161513776482, -3.941790907013290823, -0.4709369376873030477 ) ) ;
#39592=CARTESIAN_POINT ( 'NONE',  ( -0.2399999999999999079, -3.739689364820627748, -0.3461216533844236887 ) ) ;
#39598=VECTOR ( 'NONE', #22675, 39.37007874015748143 ) ;
#39622=CARTESIAN_POINT ( 'NONE',  ( -0.2746410161513776482, -4.218511633990150500, -0.6415916474861803609 ) ) ;
#39626=CARTESIAN_POINT ( 'NONE',  ( -0.2399999999999999079, -1.804235510932644004, -0.1501860188971498311 ) ) ;
#39632=ADVANCED_FACE ( 'NONE', ( #14517 ), #19516, .F. ) ;
#39637=CYLINDRICAL_SURFACE ( 'NONE', #22539, 0.6115209409081865388 ) ;
#39638=VECTOR ( 'NONE', #9438, 39.37007874015748143 ) ;
#39640=AXIS2_PLACEMENT_3D ( 'NONE', #22159, #37763, #3201 ) ;
#39649=CARTESIAN_POINT ( 'NONE',  ( -0.2399999999999999079, -3.751862894713570817, -0.4282819086714443890 ) ) ;
#39665=CARTESIAN_POINT ( 'NONE',  ( -0.2399999999999999079, -3.253295730098268113, -0.6063490597057096254 ) ) ;
#39671=CARTESIAN_POINT ( 'NONE',  ( -0.2399999999999999079, -3.933118884668405979, -0.4831760564648042711 ) ) ;
#39676=DIRECTION ( 'NONE',  ( -1.000000000000000000, -0.000000000000000000, -0.000000000000000000 ) ) ;
#39685=ADVANCED_FACE ( 'NONE', ( #29366 ), #11051, .F. ) ;
#39690=AXIS2_PLACEMENT_3D ( 'NONE', #28740, #26076, #13096 ) ;
#39699=ORIENTED_EDGE ( 'NONE', *, *, #7246, .F. ) ;
#39708=ORIENTED_EDGE ( 'NONE', *, *, #23599, .F. ) ;
#39711=DIRECTION ( 'NONE',  ( 1.000000000000000000, 0.000000000000000000, 0.000000000000000000 ) ) ;
#39715=EDGE_CURVE ( 'NONE', #28968, #20453, #4449, .T. ) ;
#39725=VECTOR ( 'NONE', #3055, 39.37007874015748143 ) ;
#39747=CIRCLE ( 'NONE', #24005, 0.1000000000000000194 ) ;
#39769=CARTESIAN_POINT ( 'NONE',  ( -0.2746410161513776482, -3.758594918004649621, -0.06617323996463200797 ) ) ;
#39775=DIRECTION ( 'NONE',  ( -1.000000000000000000, -0.000000000000000000, -0.000000000000000000 ) ) ;
#39776=DIRECTION ( 'NONE',  ( 1.000000000000000000, 0.000000000000000000, 0.000000000000000000 ) ) ;
#39800=ORIENTED_EDGE ( 'NONE', *, *, #3168, .F. ) ;
#39807=EDGE_CURVE ( 'NONE', #33695, #22635, #17012, .T. ) ;
#39819=VERTEX_POINT ( 'NONE', #26697 ) ;
#39841=AXIS2_PLACEMENT_3D ( 'NONE', #30596, #33460, #5690 ) ;
#39860=EDGE_LOOP ( 'NONE', ( #28746, #29087, #6358, #24354 ) ) ;
#39869=AXIS2_PLACEMENT_3D ( 'NONE', #23984, #17984, #30548 ) ;
#39872=VERTEX_POINT ( 'NONE', #19610 ) ;
#39874=ORIENTED_EDGE ( 'NONE', *, *, #10505, .F. ) ;
#39901=DIRECTION ( 'NONE',  ( 1.000000000000000000, -0.000000000000000000, -0.000000000000000000 ) ) ;
#39912=LINE ( 'NONE', #24703, #29653 ) ;
#39917=CARTESIAN_POINT ( 'NONE',  ( -0.2399999999999999079, -3.040459736179910166, -1.372268108520683372 ) ) ;
#39919=EDGE_CURVE ( 'NONE', #11732, #17560, #33035, .T. ) ;
#39923=DIRECTION ( 'NONE',  ( 0.000000000000000000, 0.000000000000000000, -1.000000000000000000 ) ) ;
#39992=ORIENTED_EDGE ( 'NONE', *, *, #19248, .T. ) ;
#40007=CARTESIAN_POINT ( 'NONE',  ( -0.2746410161513779258, -2.139295658456680904, -0.2024034539465678073 ) ) ;
#40011=VERTEX_POINT ( 'NONE', #2307 ) ;
#40018=CARTESIAN_POINT ( 'NONE',  ( -0.2746410161513782033, -2.323257895298838971, -0.7902071827178637209 ) ) ;
#40037=ADVANCED_FACE ( 'NONE', ( #17713 ), #1907, .T. ) ;
#40042=DIRECTION ( 'NONE',  ( 0.000000000000000000, 0.000000000000000000, -1.000000000000000000 ) ) ;
#40050=DIRECTION ( 'NONE',  ( 0.000000000000000000, 2.731847993664262824E-15, -1.000000000000000000 ) ) ;
#40051=CARTESIAN_POINT ( 'NONE',  ( -0.2399999999999999079, -4.320736256378554963, -0.8145269479932405465 ) ) ;
#40059=CARTESIAN_POINT ( 'NONE',  ( -0.2746410161513779258, -2.423474325126674156, -0.5576739111151496342 ) ) ;
#40067=CARTESIAN_POINT ( 'NONE',  ( -0.2399999999999999079, -3.318147336744930342, -0.6877918253319055264 ) ) ;
#40079=DIRECTION ( 'NONE',  ( 0.000000000000000000, 0.000000000000000000, 1.000000000000000000 ) ) ;
#40087=CARTESIAN_POINT ( 'NONE',  ( -0.2399999999999999079, -3.335205990917129881, -0.4042613180508733972 ) ) ;
#40090=ORIENTED_EDGE ( 'NONE', *, *, #35307, .T. ) ;
#40092=CIRCLE ( 'NONE', #15798, 0.1000000000000000194 ) ;
#40112=ORIENTED_EDGE ( 'NONE', *, *, #33769, .T. ) ;
#40127=CARTESIAN_POINT ( 'NONE',  ( -0.2399999999999999079, -3.941790907013290823, -0.4709369376873030477 ) ) ;
#40130=DIRECTION ( 'NONE',  ( 0.000000000000000000, 0.000000000000000000, -1.000000000000000000 ) ) ;
#40132=AXIS2_PLACEMENT_3D ( 'NONE', #17451, #4880, #36968 ) ;
#40143=DIRECTION ( 'NONE',  ( 0.000000000000000000, 0.000000000000000000, -1.000000000000000000 ) ) ;
#40147=VECTOR ( 'NONE', #4031, 39.37007874015748143 ) ;
#40157=DIRECTION ( 'NONE',  ( 0.000000000000000000, 0.000000000000000000, -1.000000000000000000 ) ) ;
#40160=VECTOR ( 'NONE', #17554, 39.37007874015748143 ) ;
#40182=AXIS2_PLACEMENT_3D ( 'NONE', #13014, #2944, #35008 ) ;
#40184=CARTESIAN_POINT ( 'NONE',  ( -0.2746410161513782033, -1.962518963160043706, -0.3791801492432049780 ) ) ;
#40185=EDGE_CURVE ( 'NONE', #38637, #22034, #20576, .T. ) ;
#40200=ORIENTED_EDGE ( 'NONE', *, *, #35990, .F. ) ;
#40208=CARTESIAN_POINT ( 'NONE',  ( -0.2399999999999999079, -1.774602679190314669, -0.1233179098656094347 ) ) ;
#40215=AXIS2_PLACEMENT_3D ( 'NONE', #7006, #14194, #19573 ) ;
#40217=CARTESIAN_POINT ( 'NONE',  ( -0.2399999999999999079, -2.407646569606659792, -0.8438593182631384249 ) ) ;
#40232=DIRECTION ( 'NONE',  ( 0.000000000000000000, 0.000000000000000000, -1.000000000000000000 ) ) ;
#40255=CARTESIAN_POINT ( 'NONE',  ( -0.2399999999999999079, -3.609310082097819894, -0.4498340178114252352 ) ) ;
#40270=LINE ( 'NONE', #30821, #27378 ) ;
#40272=VECTOR ( 'NONE', #31253, 39.37007874015748854 ) ;
#40277=ORIENTED_EDGE ( 'NONE', *, *, #32789, .T. ) ;
#40284=CIRCLE ( 'NONE', #268, 0.1000000000000000194 ) ;
#40294=CARTESIAN_POINT ( 'NONE',  ( -0.3000000000000000999, -2.109195954094405856, -0.3137251058216021793 ) ) ;
#40297=VECTOR ( 'NONE', #18507, 39.37007874015748143 ) ;
#40304=AXIS2_PLACEMENT_3D ( 'NONE', #26061, #4812, #26859 ) ;
#40318=ORIENTED_EDGE ( 'NONE', *, *, #13039, .T. ) ;
#40326=ORIENTED_EDGE ( 'NONE', *, *, #8172, .F. ) ;
#40340=VECTOR ( 'NONE', #28979, 39.37007874015748143 ) ;
#40341=CARTESIAN_POINT ( 'NONE',  ( -0.2399999999999999079, -3.196602950345407645, -0.1969487268370971322 ) ) ;
#40342=FACE_OUTER_BOUND ( 'NONE', #19978, .T. ) ;
#40350=AXIS2_PLACEMENT_3D ( 'NONE', #4914, #7997, #20574 ) ;
#40362=DIRECTION ( 'NONE',  ( 0.000000000000000000, 0.000000000000000000, -1.000000000000000000 ) ) ;
#40364=CIRCLE ( 'NONE', #32489, 0.1000000000000000194 ) ;
#40377=VERTEX_POINT ( 'NONE', #21725 ) ;
#40383=FACE_OUTER_BOUND ( 'NONE', #18066, .T. ) ;
#40401=DIRECTION ( 'NONE',  ( 1.000000000000000000, 0.000000000000000000, 0.000000000000000000 ) ) ;
#40406=EDGE_CURVE ( 'NONE', #31712, #1392, #379, .T. ) ;
#40416=ORIENTED_EDGE ( 'NONE', *, *, #21376, .F. ) ;
#40424=CARTESIAN_POINT ( 'NONE',  ( -0.3000000000000000999, -2.853330612949663170, -0.7088139570729240502 ) ) ;
#40444=CIRCLE ( 'NONE', #32534, 0.1600000000000006417 ) ;
#40460=LINE ( 'NONE', #24426, #31098 ) ;
#40462=ORIENTED_EDGE ( 'NONE', *, *, #27502, .F. ) ;
#40463=CARTESIAN_POINT ( 'NONE',  ( -0.3000000000000000999, -1.835749455202394298, -0.3938319975228649072 ) ) ;
#40466=EDGE_CURVE ( 'NONE', #32724, #32720, #38356, .T. ) ;
#40468=ADVANCED_FACE ( 'NONE', ( #35286 ), #36969, .F. ) ;
#40472=DIRECTION ( 'NONE',  ( 0.000000000000000000, 0.000000000000000000, 1.000000000000000000 ) ) ;
#40477=FACE_OUTER_BOUND ( 'NONE', #1878, .T. ) ;
#40495=DIRECTION ( 'NONE',  ( -0.4261641068392704734, 0.000000000000000000, -0.9046458721742374198 ) ) ;
#40498=LINE ( 'NONE', #11899, #35799 ) ;
#40515=CARTESIAN_POINT ( 'NONE',  ( -0.2399999999999999079, -2.853330612949663170, -0.7688139570729241035 ) ) ;
#40516=VERTEX_POINT ( 'NONE', #25215 ) ;
#40525=ORIENTED_EDGE ( 'NONE', *, *, #8751, .T. ) ;
#40527=ORIENTED_EDGE ( 'NONE', *, *, #39190, .F. ) ;
#40529=ORIENTED_EDGE ( 'NONE', *, *, #26141, .F. ) ;
#40542=DIRECTION ( 'NONE',  ( -1.000000000000000000, -0.000000000000000000, -0.000000000000000000 ) ) ;
#40544=VECTOR ( 'NONE', #19381, 39.37007874015748143 ) ;
#40547=DIRECTION ( 'NONE',  ( -0.8660254037844404840, -0.3535533905932716769, 0.3535533905932716769 ) ) ;
#40550=EDGE_CURVE ( 'NONE', #22378, #6266, #26471, .T. ) ;
#40559=EDGE_CURVE ( 'NONE', #38965, #36975, #35033, .T. ) ;
#40560=DIRECTION ( 'NONE',  ( 0.000000000000000000, 0.7071067811865474617, 0.7071067811865475727 ) ) ;
#40563=PRODUCT_DEFINITION ( 'UNKNOWN', '', #39117, #29430 ) ;
#40594=CARTESIAN_POINT ( 'NONE',  ( -0.3000000000000000999, -3.985676108854518507, -0.7623095129438225426 ) ) ;
#40595=EDGE_CURVE ( 'NONE', #12691, #12319, #35895, .T. ) ;
#40609=LINE ( 'NONE', #21301, #3546 ) ;
#40610=VERTEX_POINT ( 'NONE', #14471 ) ;
#40622=ORIENTED_EDGE ( 'NONE', *, *, #27283, .F. ) ;
#40681=COLOUR_RGB('Sky Blue',0.24,0.69,0.87);
#40682=FILL_AREA_STYLE_COLOUR('',#40681);
#40683=FILL_AREA_STYLE('',(#40682));
#40684=SURFACE_STYLE_FILL_AREA(#40683);
#40685=SURFACE_SIDE_STYLE('',(#40684));
#40686=SURFACE_STYLE_USAGE(.BOTH.,#40685);
#40687=PRESENTATION_STYLE_ASSIGNMENT((#40686));
#40716=STYLED_ITEM('',(#40687),#4819);
#40721=MECHANICAL_DESIGN_GEOMETRIC_PRESENTATION_REPRESENTATION('',(#40716),#11399);
ENDSEC;
END-ISO-10303-21;
